ISO-10303-21;
HEADER;
/* Generated by software containing ST-Developer
 * from STEP Tools, Inc. (www.steptools.com) 
 */

FILE_DESCRIPTION(
/* description */ ('Independent direct-acting normally-closed roller-plunger limit-switch
 CAD. Removable cover, insulated terminal supports, captured bus/conta
ct bridge, native Coil return spring, integral lower travel stop, reus
able instanced hardware and free roller. Manual geometric contact open
ing4mm; no snap-action/contact-force, electrical/current/voltage, envi
ronmental seal, safety-switch, wear, load or life certification. Exter
nal wiring and anchors omitted; fits and application engineering requi
red.'),
/* implementation_level */ '2;1');

FILE_NAME(
/* name */ 'Socket head cap screw M4x12.step',
/* time_stamp */ '2026-11-08T07:32:43-08:00',
/* author */ (''),
/* organization */ (''),
/* preprocessor_version */ 'ST-DEVELOPER v20.2',
/* originating_system */ 'Autodesk Translation Framework v15.17.0.0',
/* authorisation */ '');

FILE_SCHEMA (('AUTOMOTIVE_DESIGN { 1 0 10303 214 3 1 1 }'));
ENDSEC;

DATA;
#10=MECHANICAL_DESIGN_GEOMETRIC_PRESENTATION_REPRESENTATION('',(#190),#36482);
#139=CONICAL_SURFACE('',#10540,0.15,0.785398163397449);
#156=SHAPE_REPRESENTATION_RELATIONSHIP('SRR','None',#36569,#173);
#173=ADVANCED_BREP_SHAPE_REPRESENTATION('',(#207),#36479);
#190=STYLED_ITEM('',(#36659),#207);
#207=MANIFOLD_SOLID_BREP('Body1',#9781);
#229=B_SPLINE_SURFACE_WITH_KNOTS('',3,3,((#30990,#30991,#30992,#30993,#30994,
#30995,#30996,#30997,#30998,#30999,#31000,#31001,#31002,#31003,#31004,#31005,
#31006,#31007,#31008,#31009,#31010,#31011,#31012,#31013,#31014,#31015,#31016,
#31017,#31018,#31019,#31020,#31021,#31022,#31023,#31024,#31025,#31026,#31027,
#31028,#31029,#31030,#31031,#31032,#31033,#31034,#31035,#31036,#31037,#31038,
#31039,#31040,#31041,#31042,#31043,#31044,#31045,#31046,#31047,#31048,#31049,
#31050,#31051,#31052,#31053,#31054,#31055,#31056,#31057,#31058,#31059,#31060,
#31061,#31062,#31063,#31064,#31065,#31066,#31067,#31068,#31069,#31070,#31071,
#31072,#31073,#31074,#31075,#31076,#31077,#31078,#31079,#31080,#31081,#31082,
#31083,#31084,#31085,#31086,#31087,#31088,#31089,#31090,#31091,#31092,#31093,
#31094,#31095),(#31096,#31097,#31098,#31099,#31100,#31101,#31102,#31103,
#31104,#31105,#31106,#31107,#31108,#31109,#31110,#31111,#31112,#31113,#31114,
#31115,#31116,#31117,#31118,#31119,#31120,#31121,#31122,#31123,#31124,#31125,
#31126,#31127,#31128,#31129,#31130,#31131,#31132,#31133,#31134,#31135,#31136,
#31137,#31138,#31139,#31140,#31141,#31142,#31143,#31144,#31145,#31146,#31147,
#31148,#31149,#31150,#31151,#31152,#31153,#31154,#31155,#31156,#31157,#31158,
#31159,#31160,#31161,#31162,#31163,#31164,#31165,#31166,#31167,#31168,#31169,
#31170,#31171,#31172,#31173,#31174,#31175,#31176,#31177,#31178,#31179,#31180,
#31181,#31182,#31183,#31184,#31185,#31186,#31187,#31188,#31189,#31190,#31191,
#31192,#31193,#31194,#31195,#31196,#31197,#31198,#31199,#31200,#31201),
(#31202,#31203,#31204,#31205,#31206,#31207,#31208,#31209,#31210,#31211,
#31212,#31213,#31214,#31215,#31216,#31217,#31218,#31219,#31220,#31221,#31222,
#31223,#31224,#31225,#31226,#31227,#31228,#31229,#31230,#31231,#31232,#31233,
#31234,#31235,#31236,#31237,#31238,#31239,#31240,#31241,#31242,#31243,#31244,
#31245,#31246,#31247,#31248,#31249,#31250,#31251,#31252,#31253,#31254,#31255,
#31256,#31257,#31258,#31259,#31260,#31261,#31262,#31263,#31264,#31265,#31266,
#31267,#31268,#31269,#31270,#31271,#31272,#31273,#31274,#31275,#31276,#31277,
#31278,#31279,#31280,#31281,#31282,#31283,#31284,#31285,#31286,#31287,#31288,
#31289,#31290,#31291,#31292,#31293,#31294,#31295,#31296,#31297,#31298,#31299,
#31300,#31301,#31302,#31303,#31304,#31305,#31306,#31307),(#31308,#31309,
#31310,#31311,#31312,#31313,#31314,#31315,#31316,#31317,#31318,#31319,#31320,
#31321,#31322,#31323,#31324,#31325,#31326,#31327,#31328,#31329,#31330,#31331,
#31332,#31333,#31334,#31335,#31336,#31337,#31338,#31339,#31340,#31341,#31342,
#31343,#31344,#31345,#31346,#31347,#31348,#31349,#31350,#31351,#31352,#31353,
#31354,#31355,#31356,#31357,#31358,#31359,#31360,#31361,#31362,#31363,#31364,
#31365,#31366,#31367,#31368,#31369,#31370,#31371,#31372,#31373,#31374,#31375,
#31376,#31377,#31378,#31379,#31380,#31381,#31382,#31383,#31384,#31385,#31386,
#31387,#31388,#31389,#31390,#31391,#31392,#31393,#31394,#31395,#31396,#31397,
#31398,#31399,#31400,#31401,#31402,#31403,#31404,#31405,#31406,#31407,#31408,
#31409,#31410,#31411,#31412,#31413)),.UNSPECIFIED.,.F.,.F.,.F.,(4,4),(4,
1,1,1,1,1,1,1,1,1,1,1,1,1,1,1,1,1,1,1,1,1,1,1,1,1,1,1,1,1,1,1,1,1,1,1,1,
1,1,1,1,1,1,1,1,1,1,1,1,1,1,1,1,1,1,1,1,1,1,1,1,1,1,1,1,1,1,1,1,1,1,1,1,
1,1,1,1,1,1,1,1,1,1,1,1,1,1,1,1,1,1,1,1,1,1,1,1,1,1,1,1,1,1,4),(0.,0.0460148164544132),
(11.6154215191105,12.6127573616628,13.610093204215,14.6074290467673,15.6047648893195,
16.6021007318718,17.599436574424,18.5967724169762,19.5941082595285,20.5914441020807,
21.588779944633,22.5861157871852,23.5834516297375,24.5807874722897,25.5781233148419,
26.5754591573942,27.5727949999464,28.5701308424987,29.5674666850509,30.5648025276032,
31.5621383701554,32.5594742127077,33.5568100552599,34.5541458978121,35.5514817403644,
36.5488175829166,37.5461534254689,38.5434892680211,39.5408251105734,40.5381609531256,
41.5354967956779,42.5328326382301,43.5301684807823,44.5275043233346,45.5248401658868,
46.5221760084391,47.5195118509913,48.5168476935436,49.5141835360958,50.5115193786481,
51.5088552212003,52.5061910637525,53.5035269063048,54.500862748857,55.4981985914093,
56.4955344339615,57.4928702765138,58.490206119066,59.4875419616182,60.4848778041705,
61.4822136467227,62.479549489275,63.4768853318272,64.4742211743795,65.4715570169317,
66.468892859484,67.4662287020362,68.4635645445884,69.4609003871407,70.4582362296929,
71.4555720722452,72.4529079147974,73.4502437573497,74.4475795999019,75.4449154424541,
76.4422512850064,77.4395871275586,78.4369229701109,79.4342588126631,80.4315946552154,
81.4289304977676,82.4262663403199,83.4236021828721,84.4209380254243,85.4182738679766,
86.4156097105288,87.4129455530811,88.4102813956333,89.4076172381856,90.4049530807378,
91.4022889232901,92.3996247658423,93.3969606083945,94.3942964509468,95.391632293499,
96.3889681360513,97.3863039786035,98.3836398211558,99.380975663708,100.37831150626,
101.375647348812,102.372983191365,103.370319033917,104.367654876469,105.364990719021,
106.362326561574,107.359662404126,108.356998246678,109.35433408923,110.351669931783,
111.349005774335,112.346341616887,113.343677459439,114.341013301992),
 .UNSPECIFIED.);
#230=B_SPLINE_SURFACE_WITH_KNOTS('',3,3,((#31506,#31507,#31508,#31509,#31510,
#31511,#31512,#31513,#31514,#31515,#31516,#31517,#31518,#31519,#31520,#31521,
#31522,#31523,#31524,#31525,#31526,#31527,#31528,#31529,#31530,#31531,#31532,
#31533,#31534,#31535,#31536,#31537,#31538,#31539,#31540,#31541,#31542,#31543,
#31544,#31545,#31546,#31547,#31548,#31549,#31550,#31551,#31552,#31553,#31554,
#31555,#31556,#31557,#31558,#31559,#31560,#31561,#31562,#31563,#31564,#31565,
#31566,#31567,#31568,#31569,#31570,#31571,#31572,#31573,#31574,#31575,#31576,
#31577,#31578,#31579,#31580,#31581,#31582,#31583,#31584,#31585,#31586,#31587,
#31588,#31589,#31590,#31591,#31592,#31593,#31594,#31595,#31596,#31597,#31598,
#31599,#31600,#31601,#31602,#31603,#31604,#31605,#31606,#31607,#31608,#31609,
#31610,#31611,#31612,#31613),(#31614,#31615,#31616,#31617,#31618,#31619,
#31620,#31621,#31622,#31623,#31624,#31625,#31626,#31627,#31628,#31629,#31630,
#31631,#31632,#31633,#31634,#31635,#31636,#31637,#31638,#31639,#31640,#31641,
#31642,#31643,#31644,#31645,#31646,#31647,#31648,#31649,#31650,#31651,#31652,
#31653,#31654,#31655,#31656,#31657,#31658,#31659,#31660,#31661,#31662,#31663,
#31664,#31665,#31666,#31667,#31668,#31669,#31670,#31671,#31672,#31673,#31674,
#31675,#31676,#31677,#31678,#31679,#31680,#31681,#31682,#31683,#31684,#31685,
#31686,#31687,#31688,#31689,#31690,#31691,#31692,#31693,#31694,#31695,#31696,
#31697,#31698,#31699,#31700,#31701,#31702,#31703,#31704,#31705,#31706,#31707,
#31708,#31709,#31710,#31711,#31712,#31713,#31714,#31715,#31716,#31717,#31718,
#31719,#31720,#31721),(#31722,#31723,#31724,#31725,#31726,#31727,#31728,
#31729,#31730,#31731,#31732,#31733,#31734,#31735,#31736,#31737,#31738,#31739,
#31740,#31741,#31742,#31743,#31744,#31745,#31746,#31747,#31748,#31749,#31750,
#31751,#31752,#31753,#31754,#31755,#31756,#31757,#31758,#31759,#31760,#31761,
#31762,#31763,#31764,#31765,#31766,#31767,#31768,#31769,#31770,#31771,#31772,
#31773,#31774,#31775,#31776,#31777,#31778,#31779,#31780,#31781,#31782,#31783,
#31784,#31785,#31786,#31787,#31788,#31789,#31790,#31791,#31792,#31793,#31794,
#31795,#31796,#31797,#31798,#31799,#31800,#31801,#31802,#31803,#31804,#31805,
#31806,#31807,#31808,#31809,#31810,#31811,#31812,#31813,#31814,#31815,#31816,
#31817,#31818,#31819,#31820,#31821,#31822,#31823,#31824,#31825,#31826,#31827,
#31828,#31829),(#31830,#31831,#31832,#31833,#31834,#31835,#31836,#31837,
#31838,#31839,#31840,#31841,#31842,#31843,#31844,#31845,#31846,#31847,#31848,
#31849,#31850,#31851,#31852,#31853,#31854,#31855,#31856,#31857,#31858,#31859,
#31860,#31861,#31862,#31863,#31864,#31865,#31866,#31867,#31868,#31869,#31870,
#31871,#31872,#31873,#31874,#31875,#31876,#31877,#31878,#31879,#31880,#31881,
#31882,#31883,#31884,#31885,#31886,#31887,#31888,#31889,#31890,#31891,#31892,
#31893,#31894,#31895,#31896,#31897,#31898,#31899,#31900,#31901,#31902,#31903,
#31904,#31905,#31906,#31907,#31908,#31909,#31910,#31911,#31912,#31913,#31914,
#31915,#31916,#31917,#31918,#31919,#31920,#31921,#31922,#31923,#31924,#31925,
#31926,#31927,#31928,#31929,#31930,#31931,#31932,#31933,#31934,#31935,#31936,
#31937)),.UNSPECIFIED.,.F.,.F.,.F.,(4,4),(4,1,1,1,1,1,1,1,1,1,1,1,1,1,1,
1,1,1,1,1,1,1,1,1,1,1,1,1,1,1,1,1,1,1,1,1,1,1,1,1,1,1,1,1,1,1,1,1,1,1,1,
1,1,1,1,1,1,1,1,1,1,1,1,1,1,1,1,1,1,1,1,1,1,1,1,1,1,1,1,1,1,1,1,1,1,1,1,
1,1,1,1,1,1,1,1,1,1,1,1,1,1,1,1,1,1,4),(0.,0.0460148164544132),(8.31058692273969,
9.30859389336977,10.3066008639999,11.30460783463,12.30261480526,13.3006217758901,
14.2986287465202,15.2966357171503,16.2946426877804,17.2926496584105,18.2906566290406,
19.2886635996707,20.2866705703008,21.2846775409308,22.2826845115609,23.280691482191,
24.2786984528211,25.2767054234512,26.2747123940813,27.2727193647114,28.2707263353415,
29.2687333059716,30.2667402766016,31.2647472472317,32.2627542178618,33.2607611884919,
34.258768159122,35.2567751297521,36.2547821003822,37.2527890710123,38.2507960416424,
39.2488030122724,40.2468099829025,41.2448169535326,42.2428239241627,43.2408308947928,
44.2388378654229,45.236844836053,46.2348518066831,47.2328587773132,48.2308657479432,
49.2288727185733,50.2268796892034,51.2248866598335,52.2228936304636,53.2209006010937,
54.2189075717238,55.2169145423539,56.214921512984,57.212928483614,58.2109354542441,
59.2089424248742,60.2069493955043,61.2049563661344,62.2029633367645,63.2009703073946,
64.1989772780247,65.1969842486548,66.1949912192848,67.1929981899149,68.191005160545,
69.1890121311751,70.1870191018052,71.1850260724353,72.1830330430654,73.1810400136955,
74.1790469843256,75.1770539549557,76.1750609255857,77.1730678962158,78.1710748668459,
79.169081837476,80.1670888081061,81.1650957787362,82.1631027493663,83.1611097199964,
84.1591166906264,85.1571236612565,86.1551306318866,87.1531376025167,88.1511445731468,
89.1491515437769,90.147158514407,91.1451654850371,92.1431724556672,93.1411794262973,
94.1391863969273,95.1371933675574,96.1352003381875,97.1332073088176,98.1312142794477,
99.1292212500778,100.127228220708,101.125235191338,102.123242161968,103.121249132598,
104.119256103228,105.117263073858,106.115270044488,107.113277015118,108.111283985749,
109.109290956379,110.107297927009,111.105304897639,112.103311868269,113.101318838899),
 .UNSPECIFIED.);
#296=FACE_BOUND('',#1485,.T.);
#297=FACE_BOUND('',#1488,.T.);
#409=PLANE('',#10546);
#410=PLANE('',#10547);
#411=PLANE('',#10548);
#412=PLANE('',#10549);
#413=PLANE('',#10550);
#414=PLANE('',#10551);
#415=PLANE('',#10552);
#416=PLANE('',#10553);
#417=PLANE('',#10557);
#418=PLANE('',#10558);
#841=FACE_OUTER_BOUND('',#1440,.T.);
#842=FACE_OUTER_BOUND('',#1441,.T.);
#843=FACE_OUTER_BOUND('',#1442,.T.);
#844=FACE_OUTER_BOUND('',#1443,.T.);
#845=FACE_OUTER_BOUND('',#1444,.T.);
#846=FACE_OUTER_BOUND('',#1445,.T.);
#847=FACE_OUTER_BOUND('',#1446,.T.);
#848=FACE_OUTER_BOUND('',#1447,.T.);
#849=FACE_OUTER_BOUND('',#1448,.T.);
#850=FACE_OUTER_BOUND('',#1449,.T.);
#851=FACE_OUTER_BOUND('',#1450,.T.);
#852=FACE_OUTER_BOUND('',#1451,.T.);
#853=FACE_OUTER_BOUND('',#1452,.T.);
#854=FACE_OUTER_BOUND('',#1453,.T.);
#855=FACE_OUTER_BOUND('',#1454,.T.);
#856=FACE_OUTER_BOUND('',#1455,.T.);
#857=FACE_OUTER_BOUND('',#1456,.T.);
#858=FACE_OUTER_BOUND('',#1457,.T.);
#859=FACE_OUTER_BOUND('',#1458,.T.);
#860=FACE_OUTER_BOUND('',#1459,.T.);
#861=FACE_OUTER_BOUND('',#1460,.T.);
#862=FACE_OUTER_BOUND('',#1461,.T.);
#863=FACE_OUTER_BOUND('',#1462,.T.);
#864=FACE_OUTER_BOUND('',#1463,.T.);
#865=FACE_OUTER_BOUND('',#1464,.T.);
#866=FACE_OUTER_BOUND('',#1465,.T.);
#867=FACE_OUTER_BOUND('',#1466,.T.);
#868=FACE_OUTER_BOUND('',#1467,.T.);
#869=FACE_OUTER_BOUND('',#1468,.T.);
#870=FACE_OUTER_BOUND('',#1469,.T.);
#871=FACE_OUTER_BOUND('',#1470,.T.);
#872=FACE_OUTER_BOUND('',#1471,.T.);
#873=FACE_OUTER_BOUND('',#1472,.T.);
#874=FACE_OUTER_BOUND('',#1473,.T.);
#875=FACE_OUTER_BOUND('',#1474,.T.);
#876=FACE_OUTER_BOUND('',#1475,.T.);
#877=FACE_OUTER_BOUND('',#1476,.T.);
#878=FACE_OUTER_BOUND('',#1477,.T.);
#879=FACE_OUTER_BOUND('',#1478,.T.);
#880=FACE_OUTER_BOUND('',#1479,.T.);
#881=FACE_OUTER_BOUND('',#1480,.T.);
#882=FACE_OUTER_BOUND('',#1481,.T.);
#883=FACE_OUTER_BOUND('',#1482,.T.);
#884=FACE_OUTER_BOUND('',#1483,.T.);
#885=FACE_OUTER_BOUND('',#1484,.T.);
#886=FACE_OUTER_BOUND('',#1486,.T.);
#887=FACE_OUTER_BOUND('',#1487,.T.);
#888=FACE_OUTER_BOUND('',#1489,.T.);
#1440=EDGE_LOOP('',(#8116,#8117,#8118,#8119));
#1441=EDGE_LOOP('',(#8120,#8121,#8122,#8123));
#1442=EDGE_LOOP('',(#8124,#8125,#8126,#8127));
#1443=EDGE_LOOP('',(#8128,#8129,#8130,#8131));
#1444=EDGE_LOOP('',(#8132,#8133,#8134,#8135));
#1445=EDGE_LOOP('',(#8136,#8137,#8138,#8139));
#1446=EDGE_LOOP('',(#8140,#8141,#8142,#8143));
#1447=EDGE_LOOP('',(#8144,#8145,#8146,#8147));
#1448=EDGE_LOOP('',(#8148,#8149,#8150,#8151));
#1449=EDGE_LOOP('',(#8152,#8153,#8154,#8155));
#1450=EDGE_LOOP('',(#8156,#8157,#8158,#8159));
#1451=EDGE_LOOP('',(#8160,#8161,#8162,#8163));
#1452=EDGE_LOOP('',(#8164,#8165,#8166,#8167));
#1453=EDGE_LOOP('',(#8168,#8169,#8170,#8171));
#1454=EDGE_LOOP('',(#8172,#8173,#8174,#8175));
#1455=EDGE_LOOP('',(#8176,#8177,#8178,#8179));
#1456=EDGE_LOOP('',(#8180,#8181,#8182,#8183));
#1457=EDGE_LOOP('',(#8184,#8185,#8186,#8187));
#1458=EDGE_LOOP('',(#8188,#8189,#8190,#8191));
#1459=EDGE_LOOP('',(#8192,#8193,#8194,#8195));
#1460=EDGE_LOOP('',(#8196,#8197,#8198,#8199));
#1461=EDGE_LOOP('',(#8200,#8201,#8202,#8203));
#1462=EDGE_LOOP('',(#8204,#8205,#8206,#8207));
#1463=EDGE_LOOP('',(#8208,#8209,#8210,#8211));
#1464=EDGE_LOOP('',(#8212,#8213,#8214,#8215));
#1465=EDGE_LOOP('',(#8216,#8217,#8218,#8219));
#1466=EDGE_LOOP('',(#8220,#8221,#8222,#8223));
#1467=EDGE_LOOP('',(#8224,#8225,#8226,#8227));
#1468=EDGE_LOOP('',(#8228,#8229,#8230,#8231));
#1469=EDGE_LOOP('',(#8232,#8233,#8234,#8235));
#1470=EDGE_LOOP('',(#8236,#8237,#8238,#8239));
#1471=EDGE_LOOP('',(#8240,#8241,#8242,#8243));
#1472=EDGE_LOOP('',(#8244,#8245,#8246,#8247,#8248,#8249,#8250,#8251));
#1473=EDGE_LOOP('',(#8252,#8253,#8254,#8255,#8256,#8257,#8258,#8259,#8260,
#8261,#8262,#8263,#8264,#8265,#8266,#8267,#8268,#8269,#8270,#8271,#8272,
#8273,#8274,#8275,#8276,#8277,#8278,#8279,#8280,#8281,#8282,#8283,#8284,
#8285,#8286,#8287));
#1474=EDGE_LOOP('',(#8288,#8289,#8290,#8291));
#1475=EDGE_LOOP('',(#8292,#8293,#8294,#8295,#8296,#8297,#8298,#8299,#8300,
#8301,#8302,#8303,#8304,#8305,#8306,#8307,#8308,#8309,#8310,#8311,#8312,
#8313,#8314,#8315,#8316,#8317,#8318,#8319,#8320,#8321,#8322,#8323,#8324,
#8325,#8326,#8327,#8328));
#1476=EDGE_LOOP('',(#8329,#8330,#8331,#8332));
#1477=EDGE_LOOP('',(#8333,#8334,#8335,#8336));
#1478=EDGE_LOOP('',(#8337,#8338,#8339,#8340));
#1479=EDGE_LOOP('',(#8341,#8342,#8343,#8344));
#1480=EDGE_LOOP('',(#8345,#8346,#8347,#8348));
#1481=EDGE_LOOP('',(#8349,#8350,#8351,#8352));
#1482=EDGE_LOOP('',(#8353,#8354,#8355,#8356));
#1483=EDGE_LOOP('',(#8357,#8358,#8359,#8360,#8361,#8362));
#1484=EDGE_LOOP('',(#8363));
#1485=EDGE_LOOP('',(#8364,#8365,#8366,#8367));
#1486=EDGE_LOOP('',(#8368,#8369,#8370,#8371));
#1487=EDGE_LOOP('',(#8372));
#1488=EDGE_LOOP('',(#8373,#8374,#8375,#8376,#8377,#8378));
#1489=EDGE_LOOP('',(#8379));
#1717=CIRCLE('',#10507,0.1954);
#1718=CIRCLE('',#10524,0.15555);
#1719=CIRCLE('',#10541,0.1954);
#1720=CIRCLE('',#10542,0.1);
#1721=CIRCLE('',#10544,0.15555);
#1722=CIRCLE('',#10554,0.35);
#1723=CIRCLE('',#10556,0.35);
#2242=B_SPLINE_CURVE_WITH_KNOTS('',3,(#29661,#29662,#29663,#29664,#29665,
#29666,#29667,#29668,#29669,#29670),.UNSPECIFIED.,.F.,.F.,(4,3,3,4),(-4.09254174883833,
-3.98934337020898,-2.99200752765673,-2.06514013327813),.UNSPECIFIED.);
#2243=B_SPLINE_CURVE_WITH_KNOTS('',3,(#29673,#29674,#29675,#29676,#29677,
#29678,#29679),.UNSPECIFIED.,.F.,.F.,(4,3,4),(0.,0.998006970630082,1.11419103802948),
 .UNSPECIFIED.);
#2244=B_SPLINE_CURVE_WITH_KNOTS('',3,(#29684,#29685,#29686,#29687,#29688,
#29689,#29690,#29691,#29692,#29693,#29694,#29695,#29696,#29697,#29698,#29699,
#29700,#29701,#29702,#29703,#29704,#29705),.UNSPECIFIED.,.F.,.F.,(4,3,3,
3,3,3,3,4),(-10.3757270560179,-9.97335842552244,-8.9760225829702,-7.97868674041795,
-6.9813508978657,-5.98401505531347,-4.98667921276122,-4.09254174883833),
 .UNSPECIFIED.);
#2245=B_SPLINE_CURVE_WITH_KNOTS('',3,(#29706,#29707,#29708,#29709,#29710,
#29711,#29712,#29713,#29714,#29715,#29716,#29717,#29718,#29719,#29720,#29721,
#29722,#29723,#29724,#29725,#29726,#29727),.UNSPECIFIED.,.F.,.F.,(4,3,3,
3,3,3,3,4),(1.11419103802948,1.99601394126018,2.99402091189026,3.99202788252035,
4.99003485315045,5.98804182378054,6.98604879441062,7.39737634520907),
 .UNSPECIFIED.);
#2246=B_SPLINE_CURVE_WITH_KNOTS('',3,(#29732,#29733,#29734,#29735,#29736,
#29737,#29738,#29739,#29740,#29741,#29742,#29743,#29744,#29745,#29746,#29747,
#29748,#29749,#29750,#29751,#29752,#29753),.UNSPECIFIED.,.F.,.F.,(4,3,3,
3,3,3,3,4),(-16.6589123631975,-15.9573734808359,-14.9600376382837,-13.9627017957314,
-12.9653659531792,-11.9680301106269,-10.9706942680747,-10.3757270560179),
 .UNSPECIFIED.);
#2247=B_SPLINE_CURVE_WITH_KNOTS('',3,(#29754,#29755,#29756,#29757,#29758,
#29759,#29760,#29761,#29762,#29763,#29764,#29765,#29766,#29767,#29768,#29769,
#29770,#29771,#29772,#29773,#29774,#29775),.UNSPECIFIED.,.F.,.F.,(4,3,3,
3,3,3,3,4),(7.39737634520907,7.98405576504071,8.9820627356708,9.98006970630089,
10.978076676931,11.9760836475611,12.9740906181912,13.6805616523887),
 .UNSPECIFIED.);
#2248=B_SPLINE_CURVE_WITH_KNOTS('',3,(#29780,#29781,#29782,#29783,#29784,
#29785,#29786,#29787,#29788,#29789,#29790,#29791,#29792,#29793,#29794,#29795,
#29796,#29797,#29798,#29799,#29800,#29801),.UNSPECIFIED.,.F.,.F.,(4,3,3,
3,3,3,3,4),(-22.9420976703771,-21.9413885361494,-20.9440526935971,-19.9467168510449,
-18.9493810084926,-17.9520451659404,-16.9547093233881,-16.6589123631975),
 .UNSPECIFIED.);
#2249=B_SPLINE_CURVE_WITH_KNOTS('',3,(#29802,#29803,#29804,#29805,#29806,
#29807,#29808,#29809,#29810,#29811,#29812,#29813,#29814,#29815,#29816,#29817,
#29818,#29819,#29820,#29821,#29822,#29823),.UNSPECIFIED.,.F.,.F.,(4,3,3,
3,3,3,3,4),(13.6805616523887,13.9720975888212,14.9701045594513,15.9681115300814,
16.9661185007115,17.9641254713416,18.9621324419717,19.9637469595682),
 .UNSPECIFIED.);
#2250=B_SPLINE_CURVE_WITH_KNOTS('',3,(#29828,#29829,#29830,#29831,#29832,
#29833,#29834,#29835,#29836,#29837,#29838,#29839,#29840,#29841,#29842,#29843,
#29844,#29845,#29846,#29847,#29848,#29849),.UNSPECIFIED.,.F.,.F.,(4,3,3,
3,3,3,3,4),(-29.2252829775567,-28.9227394340151,-27.9254035914628,-26.9280677489106,
-25.9307319063583,-24.9333960638061,-23.9360602212539,-22.9420976703771),
 .UNSPECIFIED.);
#2251=B_SPLINE_CURVE_WITH_KNOTS('',3,(#29850,#29851,#29852,#29853,#29854,
#29855,#29856,#29857,#29858,#29859,#29860,#29861,#29862,#29863,#29864,#29865,
#29866,#29867,#29868,#29869,#29870,#29871),.UNSPECIFIED.,.F.,.F.,(4,3,3,
3,3,3,3,4),(19.9637469595682,20.9581463832319,21.956153353862,22.954160324492,
23.9521672951221,24.9501742657522,25.9481812363823,26.2469322667478),
 .UNSPECIFIED.);
#2252=B_SPLINE_CURVE_WITH_KNOTS('',3,(#29876,#29877,#29878,#29879,#29880,
#29881,#29882,#29883,#29884,#29885,#29886,#29887,#29888,#29889,#29890,#29891,
#29892,#29893,#29894,#29895,#29896,#29897),.UNSPECIFIED.,.F.,.F.,(4,3,3,
3,3,3,3,4),(-35.5084682847363,-34.9067544893285,-33.9094186467763,-32.9120828042241,
-31.9147469616718,-30.9174111191196,-29.9200752765673,-29.2252829775567),
 .UNSPECIFIED.);
#2253=B_SPLINE_CURVE_WITH_KNOTS('',3,(#29898,#29899,#29900,#29901,#29902,
#29903,#29904,#29905,#29906,#29907,#29908,#29909,#29910,#29911,#29912,#29913,
#29914,#29915,#29916,#29917,#29918,#29919),.UNSPECIFIED.,.F.,.F.,(4,3,3,
3,3,3,3,4),(26.2469322667478,26.9461882070124,27.9441951776425,28.9422021482726,
29.9402091189027,30.9382160895327,31.9362230601628,32.5301175739274),
 .UNSPECIFIED.);
#2254=B_SPLINE_CURVE_WITH_KNOTS('',3,(#29924,#29925,#29926,#29927,#29928,
#29929,#29930,#29931,#29932,#29933,#29934,#29935,#29936,#29937,#29938,#29939,
#29940,#29941,#29942,#29943,#29944,#29945),.UNSPECIFIED.,.F.,.F.,(4,3,3,
3,3,3,3,4),(-41.7916535919159,-40.890769544642,-39.8934337020898,-38.8960978595375,
-37.8987620169853,-36.901426174433,-35.9040903318808,-35.5084682847363),
 .UNSPECIFIED.);
#2255=B_SPLINE_CURVE_WITH_KNOTS('',3,(#29946,#29947,#29948,#29949,#29950,
#29951,#29952,#29953,#29954,#29955,#29956,#29957,#29958,#29959,#29960,#29961,
#29962,#29963,#29964,#29965,#29966,#29967),.UNSPECIFIED.,.F.,.F.,(4,3,3,
3,3,3,3,4),(32.5301175739274,32.9342300307929,33.932237001423,34.9302439720531,
35.9282509426832,36.9262579133133,37.9242648839434,38.813302881107),
 .UNSPECIFIED.);
#2256=B_SPLINE_CURVE_WITH_KNOTS('',3,(#29972,#29973,#29974,#29975,#29976,
#29977,#29978,#29979,#29980,#29981,#29982,#29983,#29984,#29985,#29986,#29987,
#29988,#29989,#29990,#29991,#29992,#29993,#29994,#29995,#29996),
 .UNSPECIFIED.,.F.,.F.,(4,3,3,3,3,3,3,3,4),(-48.0748388990955,-47.8721204425077,
-46.8747845999555,-45.8774487574032,-44.880112914851,-43.8827770722987,
-42.8854412297465,-41.8881053871943,-41.7916535919159),.UNSPECIFIED.);
#2257=B_SPLINE_CURVE_WITH_KNOTS('',3,(#29997,#29998,#29999,#30000,#30001,
#30002,#30003,#30004,#30005,#30006,#30007,#30008,#30009,#30010,#30011,#30012,
#30013,#30014,#30015,#30016,#30017,#30018,#30019,#30020,#30021),
 .UNSPECIFIED.,.F.,.F.,(4,3,3,3,3,3,3,3,4),(38.813302881107,38.9222718545735,
39.9202788252036,40.9182857958337,41.9162927664637,42.9142997370938,43.9123067077239,
44.910313678354,45.0964881882866),.UNSPECIFIED.);
#2258=B_SPLINE_CURVE_WITH_KNOTS('',3,(#30026,#30027,#30028,#30029,#30030,
#30031,#30032,#30033,#30034,#30035,#30036,#30037,#30038,#30039,#30040,#30041,
#30042,#30043,#30044,#30045,#30046,#30047),.UNSPECIFIED.,.F.,.F.,(4,3,3,
3,3,3,3,4),(-54.3580242062751,-53.8561354978212,-52.8587996552689,-51.8614638127167,
-50.8641279701645,-49.8667921276122,-48.86945628506,-48.0748388990955),
 .UNSPECIFIED.);
#2259=B_SPLINE_CURVE_WITH_KNOTS('',3,(#30048,#30049,#30050,#30051,#30052,
#30053,#30054,#30055,#30056,#30057,#30058,#30059,#30060,#30061,#30062,#30063,
#30064,#30065,#30066,#30067,#30068,#30069),.UNSPECIFIED.,.F.,.F.,(4,3,3,
3,3,3,3,4),(45.0964881882866,45.9083206489841,46.9063276196142,47.9043345902443,
48.9023415608744,49.9003485315045,50.8983555021345,51.3796734954662),
 .UNSPECIFIED.);
#2260=B_SPLINE_CURVE_WITH_KNOTS('',3,(#30074,#30075,#30076,#30077,#30078,
#30079,#30080,#30081,#30082,#30083,#30084,#30085,#30086,#30087,#30088,#30089,
#30090,#30091,#30092,#30093,#30094,#30095),.UNSPECIFIED.,.F.,.F.,(4,3,3,
3,3,3,3,4),(-60.6412095134546,-59.8401505531347,-58.8428147105824,-57.8454788680302,
-56.8481430254779,-55.8508071829257,-54.8534713403734,-54.3580242062751),
 .UNSPECIFIED.);
#2261=B_SPLINE_CURVE_WITH_KNOTS('',3,(#30096,#30097,#30098,#30099,#30100,
#30101,#30102,#30103,#30104,#30105,#30106,#30107,#30108,#30109,#30110,#30111,
#30112,#30113,#30114,#30115,#30116,#30117),.UNSPECIFIED.,.F.,.F.,(4,3,3,
3,3,3,3,4),(51.3796734954662,51.8963624727646,52.8943694433947,53.8923764140248,
54.8903833846549,55.888390355285,56.8863973259151,57.6628588026458),
 .UNSPECIFIED.);
#2262=B_SPLINE_CURVE_WITH_KNOTS('',3,(#30122,#30123,#30124,#30125,#30126,
#30127,#30128,#30129,#30130,#30131,#30132,#30133,#30134,#30135,#30136,#30137,
#30138,#30139,#30140,#30141,#30142,#30143,#30144,#30145,#30146),
 .UNSPECIFIED.,.F.,.F.,(4,3,3,3,3,3,3,3,4),(-66.9243948206342,-66.8215014510004,
-65.8241656084481,-64.8268297658959,-63.8294939233436,-62.8321580807914,
-61.8348222382391,-60.8374863956869,-60.6412095134546),.UNSPECIFIED.);
#2263=B_SPLINE_CURVE_WITH_KNOTS('',3,(#30147,#30148,#30149,#30150,#30151,
#30152,#30153,#30154,#30155,#30156,#30157,#30158,#30159,#30160,#30161,#30162,
#30163,#30164,#30165,#30166,#30167,#30168,#30169,#30170,#30171),
 .UNSPECIFIED.,.F.,.F.,(4,3,3,3,3,3,3,3,4),(57.6628588026458,57.8844042965452,
58.8824112671752,59.8804182378054,60.8784252084354,61.8764321790655,62.8744391496956,
63.8724461203257,63.9460441098254),.UNSPECIFIED.);
#2264=B_SPLINE_CURVE_WITH_KNOTS('',3,(#30176,#30177,#30178,#30179,#30180,
#30181,#30182,#30183,#30184,#30185,#30186,#30187,#30188,#30189,#30190,#30191,
#30192,#30193,#30194,#30195,#30196,#30197),.UNSPECIFIED.,.F.,.F.,(4,3,3,
3,3,3,3,4),(-73.2075801278138,-72.8055165063138,-71.8081806637616,-70.8108448212093,
-69.8135089786571,-68.8161731361048,-67.8188372935526,-66.9243948206342),
 .UNSPECIFIED.);
#2265=B_SPLINE_CURVE_WITH_KNOTS('',3,(#30198,#30199,#30200,#30201,#30202,
#30203,#30204,#30205,#30206,#30207,#30208,#30209,#30210,#30211,#30212,#30213,
#30214,#30215,#30216,#30217,#30218,#30219),.UNSPECIFIED.,.F.,.F.,(4,3,3,
3,3,3,3,4),(63.9460441098254,64.8704530909558,65.8684600615859,66.866467032216,
67.8644740028461,68.8624809734761,69.8604879441062,70.229229417005),
 .UNSPECIFIED.);
#2266=B_SPLINE_CURVE_WITH_KNOTS('',3,(#30224,#30225,#30226,#30227,#30228,
#30229,#30230,#30231,#30232,#30233,#30234,#30235,#30236,#30237,#30238,#30239,
#30240,#30241,#30242,#30243,#30244,#30245),.UNSPECIFIED.,.F.,.F.,(4,3,3,
3,3,3,3,4),(-79.4907654349934,-78.7895315616273,-77.792195719075,-76.7948598765228,
-75.7975240339705,-74.8001881914183,-73.802852348866,-73.2075801278138),
 .UNSPECIFIED.);
#2267=B_SPLINE_CURVE_WITH_KNOTS('',3,(#30246,#30247,#30248,#30249,#30250,
#30251,#30252,#30253,#30254,#30255,#30256,#30257,#30258,#30259,#30260,#30261,
#30262,#30263,#30264,#30265,#30266,#30267),.UNSPECIFIED.,.F.,.F.,(4,3,3,
3,3,3,3,4),(70.229229417005,70.8584949147363,71.8565018853664,72.8545088559965,
73.8525158266266,74.8505227972567,75.8485297678868,76.5124147241846),
 .UNSPECIFIED.);
#2268=B_SPLINE_CURVE_WITH_KNOTS('',3,(#30272,#30273,#30274,#30275,#30276,
#30277,#30278,#30279,#30280,#30281,#30282,#30283,#30284,#30285,#30286,#30287,
#30288,#30289,#30290,#30291,#30292,#30293),.UNSPECIFIED.,.F.,.F.,(4,3,3,
3,3,3,3,4),(-85.773950742173,-84.7735466169407,-83.7762107743885,-82.7788749318363,
-81.781539089284,-80.7842032467318,-79.7868674041795,-79.4907654349934),
 .UNSPECIFIED.);
#2269=B_SPLINE_CURVE_WITH_KNOTS('',3,(#30294,#30295,#30296,#30297,#30298,
#30299,#30300,#30301,#30302,#30303,#30304,#30305,#30306,#30307,#30308,#30309,
#30310,#30311,#30312,#30313,#30314,#30315),.UNSPECIFIED.,.F.,.F.,(4,3,3,
3,3,3,3,4),(76.5124147241846,76.8465367385169,77.8445437091469,78.842550679777,
79.8405576504071,80.8385646210372,81.8365715916673,82.7956000313642),
 .UNSPECIFIED.);
#2270=B_SPLINE_CURVE_WITH_KNOTS('',3,(#30320,#30321,#30322,#30323,#30324,
#30325,#30326,#30327,#30328,#30329,#30330,#30331,#30332,#30333,#30334,#30335,
#30336,#30337,#30338,#30339,#30340,#30341),.UNSPECIFIED.,.F.,.F.,(4,3,3,
3,3,3,3,4),(-92.0571360493526,-91.7548975148065,-90.7575616722542,-89.760225829702,
-88.7628899871497,-87.7655541445975,-86.7682183020452,-85.773950742173),
 .UNSPECIFIED.);
#2271=B_SPLINE_CURVE_WITH_KNOTS('',3,(#30342,#30343,#30344,#30345,#30346,
#30347,#30348,#30349,#30350,#30351,#30352,#30353,#30354,#30355,#30356,#30357,
#30358,#30359,#30360,#30361,#30362,#30363,#30364,#30365,#30366),
 .UNSPECIFIED.,.F.,.F.,(4,3,3,3,3,3,3,3,4),(82.7956000313642,82.8345785622974,
83.8325855329275,84.8305925035576,85.8285994741877,86.8266064448178,87.8246134154479,
88.822620386078,89.0787853385438),.UNSPECIFIED.);
#2272=B_SPLINE_CURVE_WITH_KNOTS('',3,(#30371,#30372,#30373,#30374,#30375,
#30376,#30377,#30378,#30379,#30380,#30381,#30382,#30383,#30384,#30385,#30386,
#30387,#30388,#30389,#30390,#30391,#30392),.UNSPECIFIED.,.F.,.F.,(4,3,3,
3,3,3,3,4),(-98.3403213565322,-97.7389125701199,-96.7415767275677,-95.7442408850154,
-94.7469050424632,-93.7495691999109,-92.7522333573587,-92.0571360493526),
 .UNSPECIFIED.);
#2273=B_SPLINE_CURVE_WITH_KNOTS('',3,(#30393,#30394,#30395,#30396,#30397,
#30398,#30399,#30400,#30401,#30402,#30403,#30404,#30405,#30406,#30407,#30408,
#30409,#30410,#30411,#30412,#30413,#30414),.UNSPECIFIED.,.F.,.F.,(4,3,3,
3,3,3,3,4),(89.0787853385438,89.820627356708,90.8186343273381,91.8166412979682,
92.8146482685983,93.8126552392284,94.8106622098585,95.3619706457233),
 .UNSPECIFIED.);
#2274=B_SPLINE_CURVE_WITH_KNOTS('',3,(#30420,#30421,#30422,#30423,#30424,
#30425,#30426,#30427),.UNSPECIFIED.,.F.,.F.,(4,1,1,1,1,4),(109.955742875643,
110.351669931783,111.349005774335,112.346341616887,113.343677459439,114.341013301992),
 .UNSPECIFIED.);
#2275=B_SPLINE_CURVE_WITH_KNOTS('',3,(#30430,#30431,#30432,#30433,#30434,
#30435,#30436),.UNSPECIFIED.,.F.,.F.,(4,1,1,1,4),(109.955742875643,110.107297927009,
111.105304897639,112.103311868269,113.101318838899),.UNSPECIFIED.);
#2276=B_SPLINE_CURVE_WITH_KNOTS('',3,(#30441,#30442,#30443,#30444,#30445,
#30446,#30447,#30448,#30449,#30450),.UNSPECIFIED.,.F.,.F.,(4,1,1,1,1,1,
1,4),(103.672557568463,104.367654876469,105.364990719021,106.362326561574,
107.359662404126,108.356998246678,109.35433408923,109.955742875643),
 .UNSPECIFIED.);
#2277=B_SPLINE_CURVE_WITH_KNOTS('',3,(#30451,#30452,#30453,#30454,#30455,
#30456,#30457,#30458,#30459,#30460),.UNSPECIFIED.,.F.,.F.,(4,1,1,1,1,1,
1,4),(103.672557568463,104.119256103228,105.117263073858,106.115270044488,
107.113277015118,108.111283985749,109.109290956379,109.955742875643),
 .UNSPECIFIED.);
#2278=B_SPLINE_CURVE_WITH_KNOTS('',3,(#30465,#30466,#30467,#30468,#30469,
#30470,#30471,#30472,#30473,#30474),.UNSPECIFIED.,.F.,.F.,(4,1,1,1,1,1,
1,4),(97.3893722612836,98.3836398211558,99.380975663708,100.37831150626,
101.375647348812,102.372983191365,103.370319033917,103.672557568463),
 .UNSPECIFIED.);
#2279=B_SPLINE_CURVE_WITH_KNOTS('',3,(#30475,#30476,#30477,#30478,#30479,
#30480,#30481,#30482,#30483,#30484),.UNSPECIFIED.,.F.,.F.,(4,1,1,1,1,1,
1,4),(97.3893722612836,98.1312142794477,99.1292212500778,100.127228220708,
101.125235191338,102.123242161968,103.121249132598,103.672557568463),
 .UNSPECIFIED.);
#2280=B_SPLINE_CURVE_WITH_KNOTS('',3,(#30489,#30490,#30491,#30492,#30493,
#30494,#30495,#30496,#30497,#30498,#30499),.UNSPECIFIED.,.F.,.F.,(4,1,1,
1,1,1,1,1,4),(91.106186954104,91.4022889232901,92.3996247658423,93.3969606083945,
94.3942964509468,95.391632293499,96.3889681360513,97.3863039786035,97.3893722612836),
 .UNSPECIFIED.);
#2281=B_SPLINE_CURVE_WITH_KNOTS('',3,(#30500,#30501,#30502,#30503,#30504,
#30505,#30506,#30507,#30508,#30509,#30510),.UNSPECIFIED.,.F.,.F.,(4,1,1,
1,1,1,1,1,4),(91.106186954104,91.1451654850371,92.1431724556672,93.1411794262973,
94.1391863969273,95.1371933675574,96.1352003381875,97.1332073088176,97.3893722612836),
 .UNSPECIFIED.);
#2282=B_SPLINE_CURVE_WITH_KNOTS('',3,(#30515,#30516,#30517,#30518,#30519,
#30520,#30521,#30522,#30523,#30524),.UNSPECIFIED.,.F.,.F.,(4,1,1,1,1,1,
1,4),(84.8230016469244,85.4182738679766,86.4156097105288,87.4129455530811,
88.4102813956333,89.4076172381856,90.4049530807378,91.106186954104),
 .UNSPECIFIED.);
#2283=B_SPLINE_CURVE_WITH_KNOTS('',3,(#30525,#30526,#30527,#30528,#30529,
#30530,#30531,#30532,#30533,#30534),.UNSPECIFIED.,.F.,.F.,(4,1,1,1,1,1,
1,4),(84.8230016469244,85.1571236612565,86.1551306318866,87.1531376025167,
88.1511445731468,89.1491515437769,90.147158514407,91.106186954104),
 .UNSPECIFIED.);
#2284=B_SPLINE_CURVE_WITH_KNOTS('',3,(#30539,#30540,#30541,#30542,#30543,
#30544,#30545,#30546,#30547,#30548),.UNSPECIFIED.,.F.,.F.,(4,1,1,1,1,1,
1,4),(78.5398163397448,79.4342588126631,80.4315946552154,81.4289304977676,
82.4262663403199,83.4236021828721,84.4209380254243,84.8230016469244),
 .UNSPECIFIED.);
#2285=B_SPLINE_CURVE_WITH_KNOTS('',3,(#30549,#30550,#30551,#30552,#30553,
#30554,#30555,#30556,#30557,#30558),.UNSPECIFIED.,.F.,.F.,(4,1,1,1,1,1,
1,4),(78.5398163397448,79.169081837476,80.1670888081061,81.1650957787362,
82.1631027493663,83.1611097199964,84.1591166906264,84.8230016469244),
 .UNSPECIFIED.);
#2286=B_SPLINE_CURVE_WITH_KNOTS('',3,(#30563,#30564,#30565,#30566,#30567,
#30568,#30569,#30570,#30571,#30572,#30573),.UNSPECIFIED.,.F.,.F.,(4,1,1,
1,1,1,1,1,4),(72.2566310325652,72.4529079147974,73.4502437573497,74.4475795999019,
75.4449154424541,76.4422512850064,77.4395871275586,78.4369229701109,78.5398163397448),
 .UNSPECIFIED.);
#2287=B_SPLINE_CURVE_WITH_KNOTS('',3,(#30574,#30575,#30576,#30577,#30578,
#30579,#30580,#30581,#30582,#30583),.UNSPECIFIED.,.F.,.F.,(4,1,1,1,1,1,
1,4),(72.2566310325652,73.1810400136955,74.1790469843256,75.1770539549557,
76.1750609255857,77.1730678962158,78.1710748668459,78.5398163397448),
 .UNSPECIFIED.);
#2288=B_SPLINE_CURVE_WITH_KNOTS('',3,(#30588,#30589,#30590,#30591,#30592,
#30593,#30594,#30595,#30596,#30597),.UNSPECIFIED.,.F.,.F.,(4,1,1,1,1,1,
1,4),(65.9734457253856,66.468892859484,67.4662287020362,68.4635645445884,
69.4609003871407,70.4582362296929,71.4555720722452,72.2566310325652),
 .UNSPECIFIED.);
#2289=B_SPLINE_CURVE_WITH_KNOTS('',3,(#30598,#30599,#30600,#30601,#30602,
#30603,#30604,#30605,#30606,#30607,#30608),.UNSPECIFIED.,.F.,.F.,(4,1,1,
1,1,1,1,1,4),(65.9734457253856,66.1949912192848,67.1929981899149,68.191005160545,
69.1890121311751,70.1870191018052,71.1850260724353,72.1830330430654,72.2566310325652),
 .UNSPECIFIED.);
#2290=B_SPLINE_CURVE_WITH_KNOTS('',3,(#30613,#30614,#30615,#30616,#30617,
#30618,#30619,#30620,#30621,#30622),.UNSPECIFIED.,.F.,.F.,(4,1,1,1,1,1,
1,4),(59.690260418206,60.4848778041705,61.4822136467227,62.479549489275,
63.4768853318272,64.4742211743795,65.4715570169317,65.9734457253856),
 .UNSPECIFIED.);
#2291=B_SPLINE_CURVE_WITH_KNOTS('',3,(#30623,#30624,#30625,#30626,#30627,
#30628,#30629,#30630,#30631,#30632),.UNSPECIFIED.,.F.,.F.,(4,1,1,1,1,1,
1,4),(59.690260418206,60.2069493955043,61.2049563661344,62.2029633367645,
63.2009703073946,64.1989772780247,65.1969842486548,65.9734457253856),
 .UNSPECIFIED.);
#2292=B_SPLINE_CURVE_WITH_KNOTS('',3,(#30637,#30638,#30639,#30640,#30641,
#30642,#30643,#30644,#30645,#30646,#30647),.UNSPECIFIED.,.F.,.F.,(4,1,1,
1,1,1,1,1,4),(53.4070751110265,53.5035269063048,54.500862748857,55.4981985914093,
56.4955344339615,57.4928702765138,58.490206119066,59.4875419616182,59.690260418206),
 .UNSPECIFIED.);
#2293=B_SPLINE_CURVE_WITH_KNOTS('',3,(#30648,#30649,#30650,#30651,#30652,
#30653,#30654,#30655,#30656,#30657),.UNSPECIFIED.,.F.,.F.,(4,1,1,1,1,1,
1,4),(53.4070751110264,54.2189075717238,55.2169145423539,56.214921512984,
57.212928483614,58.2109354542441,59.2089424248742,59.690260418206),
 .UNSPECIFIED.);
#2294=B_SPLINE_CURVE_WITH_KNOTS('',3,(#30662,#30663,#30664,#30665,#30666,
#30667,#30668,#30669,#30670,#30671),.UNSPECIFIED.,.F.,.F.,(4,1,1,1,1,1,
1,4),(47.1238898038469,47.5195118509913,48.5168476935436,49.5141835360958,
50.5115193786481,51.5088552212003,52.5061910637525,53.4070751110265),
 .UNSPECIFIED.);
#2295=B_SPLINE_CURVE_WITH_KNOTS('',3,(#30672,#30673,#30674,#30675,#30676,
#30677,#30678,#30679,#30680,#30681,#30682),.UNSPECIFIED.,.F.,.F.,(4,1,1,
1,1,1,1,1,4),(47.1238898038468,47.2328587773132,48.2308657479432,49.2288727185733,
50.2268796892034,51.2248866598335,52.2228936304636,53.2209006010937,53.4070751110264),
 .UNSPECIFIED.);
#2296=B_SPLINE_CURVE_WITH_KNOTS('',3,(#30687,#30688,#30689,#30690,#30691,
#30692,#30693,#30694,#30695,#30696),.UNSPECIFIED.,.F.,.F.,(4,1,1,1,1,1,
1,4),(40.8407044966673,41.5354967956779,42.5328326382301,43.5301684807823,
44.5275043233346,45.5248401658868,46.5221760084391,47.1238898038469),
 .UNSPECIFIED.);
#2297=B_SPLINE_CURVE_WITH_KNOTS('',3,(#30697,#30698,#30699,#30700,#30701,
#30702,#30703,#30704,#30705,#30706),.UNSPECIFIED.,.F.,.F.,(4,1,1,1,1,1,
1,4),(40.8407044966672,41.2448169535326,42.2428239241627,43.2408308947928,
44.2388378654229,45.236844836053,46.2348518066831,47.1238898038468),
 .UNSPECIFIED.);
#2298=B_SPLINE_CURVE_WITH_KNOTS('',3,(#30711,#30712,#30713,#30714,#30715,
#30716,#30717,#30718,#30719,#30720),.UNSPECIFIED.,.F.,.F.,(4,1,1,1,1,1,
1,4),(34.5575191894877,35.5514817403644,36.5488175829166,37.5461534254689,
38.5434892680211,39.5408251105734,40.5381609531256,40.8407044966673),
 .UNSPECIFIED.);
#2299=B_SPLINE_CURVE_WITH_KNOTS('',3,(#30721,#30722,#30723,#30724,#30725,
#30726,#30727,#30728,#30729,#30730),.UNSPECIFIED.,.F.,.F.,(4,1,1,1,1,1,
1,4),(34.5575191894876,35.2567751297521,36.2547821003822,37.2527890710123,
38.2507960416424,39.2488030122724,40.2468099829025,40.8407044966672),
 .UNSPECIFIED.);
#2300=B_SPLINE_CURVE_WITH_KNOTS('',3,(#30735,#30736,#30737,#30738,#30739,
#30740,#30741,#30742,#30743,#30744,#30745),.UNSPECIFIED.,.F.,.F.,(4,1,1,
1,1,1,1,1,4),(28.2743338823081,28.5701308424987,29.5674666850509,30.5648025276032,
31.5621383701554,32.5594742127077,33.5568100552599,34.5541458978121,34.5575191894877),
 .UNSPECIFIED.);
#2301=B_SPLINE_CURVE_WITH_KNOTS('',3,(#30746,#30747,#30748,#30749,#30750,
#30751,#30752,#30753,#30754,#30755),.UNSPECIFIED.,.F.,.F.,(4,1,1,1,1,1,
1,4),(28.274333882308,29.2687333059716,30.2667402766016,31.2647472472317,
32.2627542178618,33.2607611884919,34.258768159122,34.5575191894876),
 .UNSPECIFIED.);
#2302=B_SPLINE_CURVE_WITH_KNOTS('',3,(#30760,#30761,#30762,#30763,#30764,
#30765,#30766,#30767,#30768,#30769),.UNSPECIFIED.,.F.,.F.,(4,1,1,1,1,1,
1,4),(21.9911485751285,22.5861157871852,23.5834516297375,24.5807874722897,
25.5781233148419,26.5754591573942,27.5727949999464,28.2743338823081),
 .UNSPECIFIED.);
#2303=B_SPLINE_CURVE_WITH_KNOTS('',3,(#30770,#30771,#30772,#30773,#30774,
#30775,#30776,#30777,#30778,#30779,#30780),.UNSPECIFIED.,.F.,.F.,(4,1,1,
1,1,1,1,1,4),(21.9911485751285,22.2826845115609,23.280691482191,24.2786984528211,
25.2767054234512,26.2747123940813,27.2727193647114,28.2707263353415,28.274333882308),
 .UNSPECIFIED.);
#2304=B_SPLINE_CURVE_WITH_KNOTS('',3,(#30785,#30786,#30787,#30788,#30789,
#30790,#30791,#30792,#30793,#30794),.UNSPECIFIED.,.F.,.F.,(4,1,1,1,1,1,
1,4),(15.7079632679489,16.6021007318718,17.599436574424,18.5967724169762,
19.5941082595285,20.5914441020807,21.588779944633,21.9911485751285),
 .UNSPECIFIED.);
#2305=B_SPLINE_CURVE_WITH_KNOTS('',3,(#30795,#30796,#30797,#30798,#30799,
#30800,#30801,#30802,#30803,#30804),.UNSPECIFIED.,.F.,.F.,(4,1,1,1,1,1,
1,4),(15.7079632679489,16.2946426877804,17.2926496584105,18.2906566290406,
19.2886635996707,20.2866705703008,21.2846775409308,21.9911485751285),
 .UNSPECIFIED.);
#2306=B_SPLINE_CURVE_WITH_KNOTS('',3,(#30807,#30808,#30809,#30810,#30811,
#30812,#30813,#30814,#30815,#30816,#30817,#30818,#30819,#30820,#30821,#30822,
#30823,#30824,#30825,#30826,#30827,#30828,#30829,#30830,#30831,#30832,#30833,
#30834,#30835,#30836,#30837,#30838,#30839,#30840,#30841,#30842,#30843,#30844,
#30845,#30846,#30847,#30848,#30849,#30850,#30851,#30852,#30853,#30854,#30855,
#30856,#30857,#30858,#30859,#30860,#30861,#30862,#30863,#30864,#30865,#30866,
#30867,#30868,#30869,#30870,#30871,#30872,#30873,#30874,#30875,#30876,#30877,
#30878,#30879,#30880,#30881,#30882,#30883,#30884,#30885),.UNSPECIFIED.,
 .F.,.F.,(4,3,3,3,3,3,3,3,3,3,3,3,3,3,3,3,3,3,3,3,3,3,3,3,3,3,4),(-0.996917990983956,
-0.964197655296454,-0.951513094737375,-0.939590005196496,-0.910398139253692,
-0.896458168447615,-0.866624051431682,-0.848513043381918,-0.839276821658768,
-0.836789934415749,-0.803176729602168,-0.780362864215826,-0.769651322799483,
-0.734439153414668,-0.711686399207869,-0.700944767019061,-0.669566542377212,
-0.648981044332524,-0.637888877288902,-0.602287825523676,-0.584615028650125,
-0.570052223933311,-0.532768447080654,-0.516116381189141,-0.50154558318824,
-0.495484670227998,-0.468408511919796),.UNSPECIFIED.);
#2307=B_SPLINE_CURVE_WITH_KNOTS('',3,(#30887,#30888,#30889,#30890,#30891,
#30892,#30893,#30894,#30895,#30896,#30897,#30898,#30899,#30900,#30901,#30902,
#30903,#30904,#30905,#30906,#30907,#30908,#30909,#30910,#30911,#30912,#30913,
#30914,#30915,#30916,#30917,#30918,#30919,#30920),.UNSPECIFIED.,.F.,.F.,
(4,3,3,3,3,3,3,3,3,3,3,4),(-0.271362855059921,-0.23333358174471,-0.202109628804149,
-0.191194824123734,-0.172574372312687,-0.139871461148431,-0.130049418747569,
-0.0948265930323134,-0.0669749700089491,-0.0565955729248257,-0.0239539643597006,
0.),.UNSPECIFIED.);
#2308=B_SPLINE_CURVE_WITH_KNOTS('',3,(#30923,#30924,#30925,#30926,#30927,
#30928,#30929,#30930,#30931,#30932,#30933,#30934,#30935,#30936,#30937,#30938,
#30939,#30940,#30941,#30942,#30943,#30944,#30945,#30946,#30947,#30948,#30949,
#30950,#30951,#30952,#30953,#30954,#30955,#30956,#30957,#30958,#30959,#30960,
#30961,#30962,#30963,#30964,#30965,#30966,#30967,#30968,#30969,#30970,#30971,
#30972,#30973,#30974,#30975,#30976,#30977,#30978,#30979,#30980,#30981,#30982,
#30983,#30984,#30985,#30986),.UNSPECIFIED.,.F.,.F.,(4,3,3,3,3,3,3,3,3,3,
3,3,3,3,3,3,3,3,3,3,3,4),(-0.468408511919796,-0.44532089356327,-0.431869826400524,
-0.394574417707956,-0.377959024336246,-0.36718387876206,-0.329707820210052,
-0.314417154781481,-0.297766482794163,-0.286364248592707,-0.248901620010442,
-0.233074500624702,-0.216543640108336,-0.17799293612575,-0.152182016671258,
-0.141011423916894,-0.12652726456846,-0.094895448426345,-0.0796457512037788,
-0.0683009962329189,-0.0289678476755453,0.),.UNSPECIFIED.);
#2309=B_SPLINE_CURVE_WITH_KNOTS('',3,(#31415,#31416,#31417,#31418,#31419,
#31420,#31421,#31422),.UNSPECIFIED.,.F.,.F.,(4,1,1,1,1,4),(11.6154215191105,
12.6127573616628,13.610093204215,14.6074290467673,15.6047648893195,15.7079632679489),
 .UNSPECIFIED.);
#2310=B_SPLINE_CURVE_WITH_KNOTS('',3,(#31423,#31424,#31425,#31426,#31427,
#31428,#31429,#31430,#31431,#31432,#31433,#31434,#31435,#31436,#31437,#31438,
#31439,#31440,#31441,#31442,#31443,#31444,#31445,#31446,#31447,#31448,#31449,
#31450,#31451,#31452,#31453,#31454,#31455,#31456,#31457,#31458,#31459,#31460,
#31461,#31462,#31463,#31464,#31465,#31466,#31467,#31468,#31469,#31470,#31471,
#31472,#31473,#31474,#31475,#31476,#31477,#31478,#31479,#31480),
 .UNSPECIFIED.,.F.,.F.,(4,3,3,3,3,3,3,3,3,3,3,3,3,3,3,3,3,3,3,4),(-0.364629307890661,
-0.350885759085945,-0.324346713718219,-0.304152838893849,-0.282934787914253,
-0.264003466919189,-0.252764227803326,-0.216347623970161,-0.198031500011342,
-0.186602740018901,-0.166173598315468,-0.146000730648533,-0.128382123165429,
-0.119003916100956,-0.0892529370757172,-0.0724905256163614,-0.0619084956994276,
-0.0517443199161659,-0.0194955210690912,0.),.UNSPECIFIED.);
#2311=B_SPLINE_CURVE_WITH_KNOTS('',3,(#31481,#31482,#31483,#31484,#31485,
#31486,#31487,#31488,#31489,#31490,#31491,#31492,#31493),.UNSPECIFIED.,
 .F.,.F.,(4,3,3,3,4),(-101.213804280572,-100.730920097777,-99.7335842552244,
-98.7362484126722,-98.3403213565322),.UNSPECIFIED.);
#2312=B_SPLINE_CURVE_WITH_KNOTS('',3,(#31496,#31497,#31498,#31499,#31500,
#31501,#31502,#31503,#31504),.UNSPECIFIED.,.F.,.F.,(4,1,1,1,1,1,4),(10.3757270560178,
11.30460783463,12.30261480526,13.3006217758901,14.2986287465202,15.2966357171503,
15.7079632679489),.UNSPECIFIED.);
#2313=B_SPLINE_CURVE_WITH_KNOTS('',3,(#31938,#31939,#31940,#31941,#31942,
#31943,#31944,#31945,#31946,#31947,#31948,#31949,#31950,#31951,#31952,#31953),
 .UNSPECIFIED.,.F.,.F.,(4,3,3,3,3,4),(95.3619706457233,95.8086691804886,
96.8066761511186,97.8046831217487,98.8026900923788,99.1486641472938),
 .UNSPECIFIED.);
#2314=B_SPLINE_CURVE_WITH_KNOTS('',3,(#31954,#31955,#31956,#31957,#31958,
#31959,#31960,#31961,#31962,#31963,#31964,#31965,#31966,#31967,#31968,#31969,
#31970,#31971,#31972,#31973,#31974,#31975,#31976,#31977,#31978,#31979,#31980,
#31981,#31982,#31983,#31984,#31985,#31986,#31987,#31988,#31989,#31990,#31991,
#31992,#31993,#31994,#31995,#31996,#31997,#31998,#31999,#32000,#32001,#32002,
#32003,#32004,#32005),.UNSPECIFIED.,.F.,.F.,(4,3,3,3,3,3,3,3,3,3,3,3,3,
3,3,3,3,4),(-0.366397579005845,-0.355461226466819,-0.328804438442731,-0.31606471842091,
-0.292558951597566,-0.280250898914551,-0.245275213061006,-0.218626183485931,
-0.207947804736759,-0.187209422476688,-0.163808244667102,-0.149577787474042,
-0.13876424622794,-0.104073184670955,-0.0827908372522071,-0.0667764467402658,
-0.0282827470320728,0.),.UNSPECIFIED.);
#2871=LINE('',#29659,#3445);
#2872=LINE('',#29683,#3446);
#2873=LINE('',#29731,#3447);
#2874=LINE('',#29779,#3448);
#2875=LINE('',#29827,#3449);
#2876=LINE('',#29875,#3450);
#2877=LINE('',#29923,#3451);
#2878=LINE('',#29971,#3452);
#2879=LINE('',#30025,#3453);
#2880=LINE('',#30073,#3454);
#2881=LINE('',#30121,#3455);
#2882=LINE('',#30175,#3456);
#2883=LINE('',#30223,#3457);
#2884=LINE('',#30271,#3458);
#2885=LINE('',#30319,#3459);
#2886=LINE('',#30370,#3460);
#2887=LINE('',#30418,#3461);
#2888=LINE('',#30440,#3462);
#2889=LINE('',#30464,#3463);
#2890=LINE('',#30488,#3464);
#2891=LINE('',#30514,#3465);
#2892=LINE('',#30538,#3466);
#2893=LINE('',#30562,#3467);
#2894=LINE('',#30587,#3468);
#2895=LINE('',#30612,#3469);
#2896=LINE('',#30636,#3470);
#2897=LINE('',#30661,#3471);
#2898=LINE('',#30686,#3472);
#2899=LINE('',#30710,#3473);
#2900=LINE('',#30734,#3474);
#2901=LINE('',#30759,#3475);
#2902=LINE('',#30784,#3476);
#2903=LINE('',#30988,#3477);
#2904=LINE('',#32010,#3478);
#2905=LINE('',#32012,#3479);
#2906=LINE('',#32014,#3480);
#2907=LINE('',#32015,#3481);
#2908=LINE('',#32018,#3482);
#2909=LINE('',#32020,#3483);
#2910=LINE('',#32021,#3484);
#2911=LINE('',#32024,#3485);
#2912=LINE('',#32026,#3486);
#2913=LINE('',#32027,#3487);
#2914=LINE('',#32030,#3488);
#2915=LINE('',#32032,#3489);
#2916=LINE('',#32033,#3490);
#2917=LINE('',#32036,#3491);
#2918=LINE('',#32038,#3492);
#2919=LINE('',#32039,#3493);
#2920=LINE('',#32041,#3494);
#2921=LINE('',#32042,#3495);
#2922=LINE('',#32049,#3496);
#3445=VECTOR('',#12186,0.2);
#3446=VECTOR('',#12191,0.2);
#3447=VECTOR('',#12194,0.2);
#3448=VECTOR('',#12197,0.2);
#3449=VECTOR('',#12200,0.2);
#3450=VECTOR('',#12203,0.2);
#3451=VECTOR('',#12206,0.2);
#3452=VECTOR('',#12209,0.2);
#3453=VECTOR('',#12212,0.2);
#3454=VECTOR('',#12215,0.2);
#3455=VECTOR('',#12218,0.2);
#3456=VECTOR('',#12221,0.2);
#3457=VECTOR('',#12224,0.2);
#3458=VECTOR('',#12227,0.2);
#3459=VECTOR('',#12230,0.2);
#3460=VECTOR('',#12233,0.2);
#3461=VECTOR('',#12236,0.15555);
#3462=VECTOR('',#12241,0.15555);
#3463=VECTOR('',#12244,0.15555);
#3464=VECTOR('',#12247,0.15555);
#3465=VECTOR('',#12250,0.15555);
#3466=VECTOR('',#12253,0.15555);
#3467=VECTOR('',#12256,0.15555);
#3468=VECTOR('',#12259,0.15555);
#3469=VECTOR('',#12262,0.15555);
#3470=VECTOR('',#12265,0.15555);
#3471=VECTOR('',#12268,0.15555);
#3472=VECTOR('',#12271,0.15555);
#3473=VECTOR('',#12274,0.15555);
#3474=VECTOR('',#12277,0.15555);
#3475=VECTOR('',#12280,0.15555);
#3476=VECTOR('',#12283,0.15555);
#3477=VECTOR('',#12288,0.15);
#3478=VECTOR('',#12299,1.);
#3479=VECTOR('',#12300,1.);
#3480=VECTOR('',#12301,1.);
#3481=VECTOR('',#12302,1.);
#3482=VECTOR('',#12305,1.);
#3483=VECTOR('',#12306,1.);
#3484=VECTOR('',#12307,1.);
#3485=VECTOR('',#12310,1.);
#3486=VECTOR('',#12311,1.);
#3487=VECTOR('',#12312,1.);
#3488=VECTOR('',#12315,1.);
#3489=VECTOR('',#12316,1.);
#3490=VECTOR('',#12317,1.);
#3491=VECTOR('',#12320,1.);
#3492=VECTOR('',#12321,1.);
#3493=VECTOR('',#12322,1.);
#3494=VECTOR('',#12325,1.);
#3495=VECTOR('',#12326,1.);
#3496=VECTOR('',#12335,0.35);
#4301=VERTEX_POINT('',#29657);
#4302=VERTEX_POINT('',#29658);
#4303=VERTEX_POINT('',#29660);
#4304=VERTEX_POINT('',#29671);
#4305=VERTEX_POINT('',#29681);
#4306=VERTEX_POINT('',#29682);
#4307=VERTEX_POINT('',#29729);
#4308=VERTEX_POINT('',#29730);
#4309=VERTEX_POINT('',#29777);
#4310=VERTEX_POINT('',#29778);
#4311=VERTEX_POINT('',#29825);
#4312=VERTEX_POINT('',#29826);
#4313=VERTEX_POINT('',#29873);
#4314=VERTEX_POINT('',#29874);
#4315=VERTEX_POINT('',#29921);
#4316=VERTEX_POINT('',#29922);
#4317=VERTEX_POINT('',#29969);
#4318=VERTEX_POINT('',#29970);
#4319=VERTEX_POINT('',#30023);
#4320=VERTEX_POINT('',#30024);
#4321=VERTEX_POINT('',#30071);
#4322=VERTEX_POINT('',#30072);
#4323=VERTEX_POINT('',#30119);
#4324=VERTEX_POINT('',#30120);
#4325=VERTEX_POINT('',#30173);
#4326=VERTEX_POINT('',#30174);
#4327=VERTEX_POINT('',#30221);
#4328=VERTEX_POINT('',#30222);
#4329=VERTEX_POINT('',#30269);
#4330=VERTEX_POINT('',#30270);
#4331=VERTEX_POINT('',#30317);
#4332=VERTEX_POINT('',#30318);
#4333=VERTEX_POINT('',#30368);
#4334=VERTEX_POINT('',#30369);
#4335=VERTEX_POINT('',#30416);
#4336=VERTEX_POINT('',#30417);
#4337=VERTEX_POINT('',#30419);
#4338=VERTEX_POINT('',#30428);
#4339=VERTEX_POINT('',#30438);
#4340=VERTEX_POINT('',#30439);
#4341=VERTEX_POINT('',#30462);
#4342=VERTEX_POINT('',#30463);
#4343=VERTEX_POINT('',#30486);
#4344=VERTEX_POINT('',#30487);
#4345=VERTEX_POINT('',#30512);
#4346=VERTEX_POINT('',#30513);
#4347=VERTEX_POINT('',#30536);
#4348=VERTEX_POINT('',#30537);
#4349=VERTEX_POINT('',#30560);
#4350=VERTEX_POINT('',#30561);
#4351=VERTEX_POINT('',#30585);
#4352=VERTEX_POINT('',#30586);
#4353=VERTEX_POINT('',#30610);
#4354=VERTEX_POINT('',#30611);
#4355=VERTEX_POINT('',#30634);
#4356=VERTEX_POINT('',#30635);
#4357=VERTEX_POINT('',#30659);
#4358=VERTEX_POINT('',#30660);
#4359=VERTEX_POINT('',#30684);
#4360=VERTEX_POINT('',#30685);
#4361=VERTEX_POINT('',#30708);
#4362=VERTEX_POINT('',#30709);
#4363=VERTEX_POINT('',#30732);
#4364=VERTEX_POINT('',#30733);
#4365=VERTEX_POINT('',#30757);
#4366=VERTEX_POINT('',#30758);
#4367=VERTEX_POINT('',#30782);
#4368=VERTEX_POINT('',#30783);
#4369=VERTEX_POINT('',#30806);
#4370=VERTEX_POINT('',#30886);
#4371=VERTEX_POINT('',#30921);
#4372=VERTEX_POINT('',#30987);
#4373=VERTEX_POINT('',#31414);
#4374=VERTEX_POINT('',#31495);
#4375=VERTEX_POINT('',#32008);
#4376=VERTEX_POINT('',#32009);
#4377=VERTEX_POINT('',#32011);
#4378=VERTEX_POINT('',#32013);
#4379=VERTEX_POINT('',#32017);
#4380=VERTEX_POINT('',#32019);
#4381=VERTEX_POINT('',#32023);
#4382=VERTEX_POINT('',#32025);
#4383=VERTEX_POINT('',#32029);
#4384=VERTEX_POINT('',#32031);
#4385=VERTEX_POINT('',#32035);
#4386=VERTEX_POINT('',#32037);
#4387=VERTEX_POINT('',#32045);
#4388=VERTEX_POINT('',#32048);
#5614=EDGE_CURVE('',#4301,#4302,#2871,.T.);
#5615=EDGE_CURVE('',#4301,#4303,#2242,.T.);
#5616=EDGE_CURVE('',#4303,#4304,#1717,.F.);
#5617=EDGE_CURVE('',#4304,#4302,#2243,.T.);
#5618=EDGE_CURVE('',#4305,#4306,#2872,.T.);
#5619=EDGE_CURVE('',#4305,#4301,#2244,.T.);
#5620=EDGE_CURVE('',#4302,#4306,#2245,.T.);
#5621=EDGE_CURVE('',#4307,#4308,#2873,.T.);
#5622=EDGE_CURVE('',#4307,#4305,#2246,.T.);
#5623=EDGE_CURVE('',#4306,#4308,#2247,.T.);
#5624=EDGE_CURVE('',#4309,#4310,#2874,.T.);
#5625=EDGE_CURVE('',#4309,#4307,#2248,.T.);
#5626=EDGE_CURVE('',#4308,#4310,#2249,.T.);
#5627=EDGE_CURVE('',#4311,#4312,#2875,.T.);
#5628=EDGE_CURVE('',#4311,#4309,#2250,.T.);
#5629=EDGE_CURVE('',#4310,#4312,#2251,.T.);
#5630=EDGE_CURVE('',#4313,#4314,#2876,.T.);
#5631=EDGE_CURVE('',#4313,#4311,#2252,.T.);
#5632=EDGE_CURVE('',#4312,#4314,#2253,.T.);
#5633=EDGE_CURVE('',#4315,#4316,#2877,.T.);
#5634=EDGE_CURVE('',#4315,#4313,#2254,.T.);
#5635=EDGE_CURVE('',#4314,#4316,#2255,.T.);
#5636=EDGE_CURVE('',#4317,#4318,#2878,.T.);
#5637=EDGE_CURVE('',#4317,#4315,#2256,.T.);
#5638=EDGE_CURVE('',#4316,#4318,#2257,.T.);
#5639=EDGE_CURVE('',#4319,#4320,#2879,.T.);
#5640=EDGE_CURVE('',#4319,#4317,#2258,.T.);
#5641=EDGE_CURVE('',#4318,#4320,#2259,.T.);
#5642=EDGE_CURVE('',#4321,#4322,#2880,.T.);
#5643=EDGE_CURVE('',#4321,#4319,#2260,.T.);
#5644=EDGE_CURVE('',#4320,#4322,#2261,.T.);
#5645=EDGE_CURVE('',#4323,#4324,#2881,.T.);
#5646=EDGE_CURVE('',#4323,#4321,#2262,.T.);
#5647=EDGE_CURVE('',#4322,#4324,#2263,.T.);
#5648=EDGE_CURVE('',#4325,#4326,#2882,.T.);
#5649=EDGE_CURVE('',#4325,#4323,#2264,.T.);
#5650=EDGE_CURVE('',#4324,#4326,#2265,.T.);
#5651=EDGE_CURVE('',#4327,#4328,#2883,.T.);
#5652=EDGE_CURVE('',#4327,#4325,#2266,.T.);
#5653=EDGE_CURVE('',#4326,#4328,#2267,.T.);
#5654=EDGE_CURVE('',#4329,#4330,#2884,.T.);
#5655=EDGE_CURVE('',#4329,#4327,#2268,.T.);
#5656=EDGE_CURVE('',#4328,#4330,#2269,.T.);
#5657=EDGE_CURVE('',#4331,#4332,#2885,.T.);
#5658=EDGE_CURVE('',#4331,#4329,#2270,.T.);
#5659=EDGE_CURVE('',#4330,#4332,#2271,.T.);
#5660=EDGE_CURVE('',#4333,#4334,#2886,.T.);
#5661=EDGE_CURVE('',#4333,#4331,#2272,.T.);
#5662=EDGE_CURVE('',#4332,#4334,#2273,.T.);
#5663=EDGE_CURVE('',#4335,#4336,#2887,.T.);
#5664=EDGE_CURVE('',#4335,#4337,#2274,.T.);
#5665=EDGE_CURVE('',#4337,#4338,#1718,.T.);
#5666=EDGE_CURVE('',#4336,#4338,#2275,.T.);
#5667=EDGE_CURVE('',#4339,#4340,#2888,.T.);
#5668=EDGE_CURVE('',#4339,#4335,#2276,.T.);
#5669=EDGE_CURVE('',#4340,#4336,#2277,.T.);
#5670=EDGE_CURVE('',#4341,#4342,#2889,.T.);
#5671=EDGE_CURVE('',#4341,#4339,#2278,.T.);
#5672=EDGE_CURVE('',#4342,#4340,#2279,.T.);
#5673=EDGE_CURVE('',#4343,#4344,#2890,.T.);
#5674=EDGE_CURVE('',#4343,#4341,#2280,.T.);
#5675=EDGE_CURVE('',#4344,#4342,#2281,.T.);
#5676=EDGE_CURVE('',#4345,#4346,#2891,.T.);
#5677=EDGE_CURVE('',#4345,#4343,#2282,.T.);
#5678=EDGE_CURVE('',#4346,#4344,#2283,.T.);
#5679=EDGE_CURVE('',#4347,#4348,#2892,.T.);
#5680=EDGE_CURVE('',#4347,#4345,#2284,.T.);
#5681=EDGE_CURVE('',#4348,#4346,#2285,.T.);
#5682=EDGE_CURVE('',#4349,#4350,#2893,.T.);
#5683=EDGE_CURVE('',#4349,#4347,#2286,.T.);
#5684=EDGE_CURVE('',#4350,#4348,#2287,.T.);
#5685=EDGE_CURVE('',#4351,#4352,#2894,.T.);
#5686=EDGE_CURVE('',#4351,#4349,#2288,.T.);
#5687=EDGE_CURVE('',#4352,#4350,#2289,.T.);
#5688=EDGE_CURVE('',#4353,#4354,#2895,.T.);
#5689=EDGE_CURVE('',#4353,#4351,#2290,.T.);
#5690=EDGE_CURVE('',#4354,#4352,#2291,.T.);
#5691=EDGE_CURVE('',#4355,#4356,#2896,.T.);
#5692=EDGE_CURVE('',#4355,#4353,#2292,.T.);
#5693=EDGE_CURVE('',#4356,#4354,#2293,.T.);
#5694=EDGE_CURVE('',#4357,#4358,#2897,.T.);
#5695=EDGE_CURVE('',#4357,#4355,#2294,.T.);
#5696=EDGE_CURVE('',#4358,#4356,#2295,.T.);
#5697=EDGE_CURVE('',#4359,#4360,#2898,.T.);
#5698=EDGE_CURVE('',#4359,#4357,#2296,.T.);
#5699=EDGE_CURVE('',#4360,#4358,#2297,.T.);
#5700=EDGE_CURVE('',#4361,#4362,#2899,.T.);
#5701=EDGE_CURVE('',#4361,#4359,#2298,.T.);
#5702=EDGE_CURVE('',#4362,#4360,#2299,.T.);
#5703=EDGE_CURVE('',#4363,#4364,#2900,.T.);
#5704=EDGE_CURVE('',#4363,#4361,#2300,.T.);
#5705=EDGE_CURVE('',#4364,#4362,#2301,.T.);
#5706=EDGE_CURVE('',#4365,#4366,#2901,.T.);
#5707=EDGE_CURVE('',#4365,#4363,#2302,.T.);
#5708=EDGE_CURVE('',#4366,#4364,#2303,.T.);
#5709=EDGE_CURVE('',#4367,#4368,#2902,.T.);
#5710=EDGE_CURVE('',#4367,#4365,#2304,.T.);
#5711=EDGE_CURVE('',#4368,#4366,#2305,.T.);
#5712=EDGE_CURVE('',#4338,#4369,#2306,.T.);
#5713=EDGE_CURVE('',#4370,#4337,#2307,.T.);
#5714=EDGE_CURVE('',#4371,#4370,#1719,.T.);
#5715=EDGE_CURVE('',#4369,#4371,#2308,.T.);
#5716=EDGE_CURVE('',#4369,#4372,#2903,.T.);
#5717=EDGE_CURVE('',#4372,#4372,#1720,.T.);
#5718=EDGE_CURVE('',#4373,#4367,#2309,.T.);
#5719=EDGE_CURVE('',#4303,#4373,#2310,.T.);
#5720=EDGE_CURVE('',#4370,#4333,#2311,.T.);
#5721=EDGE_CURVE('',#4374,#4368,#2312,.T.);
#5722=EDGE_CURVE('',#4373,#4374,#1721,.T.);
#5723=EDGE_CURVE('',#4334,#4371,#2313,.T.);
#5724=EDGE_CURVE('',#4374,#4304,#2314,.T.);
#5725=EDGE_CURVE('',#4375,#4376,#2904,.T.);
#5726=EDGE_CURVE('',#4375,#4377,#2905,.T.);
#5727=EDGE_CURVE('',#4377,#4378,#2906,.T.);
#5728=EDGE_CURVE('',#4376,#4378,#2907,.T.);
#5729=EDGE_CURVE('',#4379,#4375,#2908,.T.);
#5730=EDGE_CURVE('',#4379,#4380,#2909,.T.);
#5731=EDGE_CURVE('',#4380,#4377,#2910,.T.);
#5732=EDGE_CURVE('',#4381,#4379,#2911,.T.);
#5733=EDGE_CURVE('',#4381,#4382,#2912,.T.);
#5734=EDGE_CURVE('',#4382,#4380,#2913,.T.);
#5735=EDGE_CURVE('',#4383,#4381,#2914,.T.);
#5736=EDGE_CURVE('',#4383,#4384,#2915,.T.);
#5737=EDGE_CURVE('',#4384,#4382,#2916,.T.);
#5738=EDGE_CURVE('',#4385,#4383,#2917,.T.);
#5739=EDGE_CURVE('',#4385,#4386,#2918,.T.);
#5740=EDGE_CURVE('',#4386,#4384,#2919,.T.);
#5741=EDGE_CURVE('',#4376,#4385,#2920,.T.);
#5742=EDGE_CURVE('',#4378,#4386,#2921,.T.);
#5743=EDGE_CURVE('',#4387,#4387,#1722,.T.);
#5744=EDGE_CURVE('',#4387,#4388,#2922,.T.);
#5745=EDGE_CURVE('',#4388,#4388,#1723,.T.);
#8116=ORIENTED_EDGE('',*,*,#5614,.F.);
#8117=ORIENTED_EDGE('',*,*,#5615,.T.);
#8118=ORIENTED_EDGE('',*,*,#5616,.T.);
#8119=ORIENTED_EDGE('',*,*,#5617,.T.);
#8120=ORIENTED_EDGE('',*,*,#5618,.F.);
#8121=ORIENTED_EDGE('',*,*,#5619,.T.);
#8122=ORIENTED_EDGE('',*,*,#5614,.T.);
#8123=ORIENTED_EDGE('',*,*,#5620,.T.);
#8124=ORIENTED_EDGE('',*,*,#5621,.F.);
#8125=ORIENTED_EDGE('',*,*,#5622,.T.);
#8126=ORIENTED_EDGE('',*,*,#5618,.T.);
#8127=ORIENTED_EDGE('',*,*,#5623,.T.);
#8128=ORIENTED_EDGE('',*,*,#5624,.F.);
#8129=ORIENTED_EDGE('',*,*,#5625,.T.);
#8130=ORIENTED_EDGE('',*,*,#5621,.T.);
#8131=ORIENTED_EDGE('',*,*,#5626,.T.);
#8132=ORIENTED_EDGE('',*,*,#5627,.F.);
#8133=ORIENTED_EDGE('',*,*,#5628,.T.);
#8134=ORIENTED_EDGE('',*,*,#5624,.T.);
#8135=ORIENTED_EDGE('',*,*,#5629,.T.);
#8136=ORIENTED_EDGE('',*,*,#5630,.F.);
#8137=ORIENTED_EDGE('',*,*,#5631,.T.);
#8138=ORIENTED_EDGE('',*,*,#5627,.T.);
#8139=ORIENTED_EDGE('',*,*,#5632,.T.);
#8140=ORIENTED_EDGE('',*,*,#5633,.F.);
#8141=ORIENTED_EDGE('',*,*,#5634,.T.);
#8142=ORIENTED_EDGE('',*,*,#5630,.T.);
#8143=ORIENTED_EDGE('',*,*,#5635,.T.);
#8144=ORIENTED_EDGE('',*,*,#5636,.F.);
#8145=ORIENTED_EDGE('',*,*,#5637,.T.);
#8146=ORIENTED_EDGE('',*,*,#5633,.T.);
#8147=ORIENTED_EDGE('',*,*,#5638,.T.);
#8148=ORIENTED_EDGE('',*,*,#5639,.F.);
#8149=ORIENTED_EDGE('',*,*,#5640,.T.);
#8150=ORIENTED_EDGE('',*,*,#5636,.T.);
#8151=ORIENTED_EDGE('',*,*,#5641,.T.);
#8152=ORIENTED_EDGE('',*,*,#5642,.F.);
#8153=ORIENTED_EDGE('',*,*,#5643,.T.);
#8154=ORIENTED_EDGE('',*,*,#5639,.T.);
#8155=ORIENTED_EDGE('',*,*,#5644,.T.);
#8156=ORIENTED_EDGE('',*,*,#5645,.F.);
#8157=ORIENTED_EDGE('',*,*,#5646,.T.);
#8158=ORIENTED_EDGE('',*,*,#5642,.T.);
#8159=ORIENTED_EDGE('',*,*,#5647,.T.);
#8160=ORIENTED_EDGE('',*,*,#5648,.F.);
#8161=ORIENTED_EDGE('',*,*,#5649,.T.);
#8162=ORIENTED_EDGE('',*,*,#5645,.T.);
#8163=ORIENTED_EDGE('',*,*,#5650,.T.);
#8164=ORIENTED_EDGE('',*,*,#5651,.F.);
#8165=ORIENTED_EDGE('',*,*,#5652,.T.);
#8166=ORIENTED_EDGE('',*,*,#5648,.T.);
#8167=ORIENTED_EDGE('',*,*,#5653,.T.);
#8168=ORIENTED_EDGE('',*,*,#5654,.F.);
#8169=ORIENTED_EDGE('',*,*,#5655,.T.);
#8170=ORIENTED_EDGE('',*,*,#5651,.T.);
#8171=ORIENTED_EDGE('',*,*,#5656,.T.);
#8172=ORIENTED_EDGE('',*,*,#5657,.F.);
#8173=ORIENTED_EDGE('',*,*,#5658,.T.);
#8174=ORIENTED_EDGE('',*,*,#5654,.T.);
#8175=ORIENTED_EDGE('',*,*,#5659,.T.);
#8176=ORIENTED_EDGE('',*,*,#5660,.F.);
#8177=ORIENTED_EDGE('',*,*,#5661,.T.);
#8178=ORIENTED_EDGE('',*,*,#5657,.T.);
#8179=ORIENTED_EDGE('',*,*,#5662,.T.);
#8180=ORIENTED_EDGE('',*,*,#5663,.F.);
#8181=ORIENTED_EDGE('',*,*,#5664,.T.);
#8182=ORIENTED_EDGE('',*,*,#5665,.T.);
#8183=ORIENTED_EDGE('',*,*,#5666,.F.);
#8184=ORIENTED_EDGE('',*,*,#5667,.F.);
#8185=ORIENTED_EDGE('',*,*,#5668,.T.);
#8186=ORIENTED_EDGE('',*,*,#5663,.T.);
#8187=ORIENTED_EDGE('',*,*,#5669,.F.);
#8188=ORIENTED_EDGE('',*,*,#5670,.F.);
#8189=ORIENTED_EDGE('',*,*,#5671,.T.);
#8190=ORIENTED_EDGE('',*,*,#5667,.T.);
#8191=ORIENTED_EDGE('',*,*,#5672,.F.);
#8192=ORIENTED_EDGE('',*,*,#5673,.F.);
#8193=ORIENTED_EDGE('',*,*,#5674,.T.);
#8194=ORIENTED_EDGE('',*,*,#5670,.T.);
#8195=ORIENTED_EDGE('',*,*,#5675,.F.);
#8196=ORIENTED_EDGE('',*,*,#5676,.F.);
#8197=ORIENTED_EDGE('',*,*,#5677,.T.);
#8198=ORIENTED_EDGE('',*,*,#5673,.T.);
#8199=ORIENTED_EDGE('',*,*,#5678,.F.);
#8200=ORIENTED_EDGE('',*,*,#5679,.F.);
#8201=ORIENTED_EDGE('',*,*,#5680,.T.);
#8202=ORIENTED_EDGE('',*,*,#5676,.T.);
#8203=ORIENTED_EDGE('',*,*,#5681,.F.);
#8204=ORIENTED_EDGE('',*,*,#5682,.F.);
#8205=ORIENTED_EDGE('',*,*,#5683,.T.);
#8206=ORIENTED_EDGE('',*,*,#5679,.T.);
#8207=ORIENTED_EDGE('',*,*,#5684,.F.);
#8208=ORIENTED_EDGE('',*,*,#5685,.F.);
#8209=ORIENTED_EDGE('',*,*,#5686,.T.);
#8210=ORIENTED_EDGE('',*,*,#5682,.T.);
#8211=ORIENTED_EDGE('',*,*,#5687,.F.);
#8212=ORIENTED_EDGE('',*,*,#5688,.F.);
#8213=ORIENTED_EDGE('',*,*,#5689,.T.);
#8214=ORIENTED_EDGE('',*,*,#5685,.T.);
#8215=ORIENTED_EDGE('',*,*,#5690,.F.);
#8216=ORIENTED_EDGE('',*,*,#5691,.F.);
#8217=ORIENTED_EDGE('',*,*,#5692,.T.);
#8218=ORIENTED_EDGE('',*,*,#5688,.T.);
#8219=ORIENTED_EDGE('',*,*,#5693,.F.);
#8220=ORIENTED_EDGE('',*,*,#5694,.F.);
#8221=ORIENTED_EDGE('',*,*,#5695,.T.);
#8222=ORIENTED_EDGE('',*,*,#5691,.T.);
#8223=ORIENTED_EDGE('',*,*,#5696,.F.);
#8224=ORIENTED_EDGE('',*,*,#5697,.F.);
#8225=ORIENTED_EDGE('',*,*,#5698,.T.);
#8226=ORIENTED_EDGE('',*,*,#5694,.T.);
#8227=ORIENTED_EDGE('',*,*,#5699,.F.);
#8228=ORIENTED_EDGE('',*,*,#5700,.F.);
#8229=ORIENTED_EDGE('',*,*,#5701,.T.);
#8230=ORIENTED_EDGE('',*,*,#5697,.T.);
#8231=ORIENTED_EDGE('',*,*,#5702,.F.);
#8232=ORIENTED_EDGE('',*,*,#5703,.F.);
#8233=ORIENTED_EDGE('',*,*,#5704,.T.);
#8234=ORIENTED_EDGE('',*,*,#5700,.T.);
#8235=ORIENTED_EDGE('',*,*,#5705,.F.);
#8236=ORIENTED_EDGE('',*,*,#5706,.F.);
#8237=ORIENTED_EDGE('',*,*,#5707,.T.);
#8238=ORIENTED_EDGE('',*,*,#5703,.T.);
#8239=ORIENTED_EDGE('',*,*,#5708,.F.);
#8240=ORIENTED_EDGE('',*,*,#5709,.F.);
#8241=ORIENTED_EDGE('',*,*,#5710,.T.);
#8242=ORIENTED_EDGE('',*,*,#5706,.T.);
#8243=ORIENTED_EDGE('',*,*,#5711,.F.);
#8244=ORIENTED_EDGE('',*,*,#5712,.F.);
#8245=ORIENTED_EDGE('',*,*,#5665,.F.);
#8246=ORIENTED_EDGE('',*,*,#5713,.F.);
#8247=ORIENTED_EDGE('',*,*,#5714,.F.);
#8248=ORIENTED_EDGE('',*,*,#5715,.F.);
#8249=ORIENTED_EDGE('',*,*,#5716,.T.);
#8250=ORIENTED_EDGE('',*,*,#5717,.F.);
#8251=ORIENTED_EDGE('',*,*,#5716,.F.);
#8252=ORIENTED_EDGE('',*,*,#5713,.T.);
#8253=ORIENTED_EDGE('',*,*,#5664,.F.);
#8254=ORIENTED_EDGE('',*,*,#5668,.F.);
#8255=ORIENTED_EDGE('',*,*,#5671,.F.);
#8256=ORIENTED_EDGE('',*,*,#5674,.F.);
#8257=ORIENTED_EDGE('',*,*,#5677,.F.);
#8258=ORIENTED_EDGE('',*,*,#5680,.F.);
#8259=ORIENTED_EDGE('',*,*,#5683,.F.);
#8260=ORIENTED_EDGE('',*,*,#5686,.F.);
#8261=ORIENTED_EDGE('',*,*,#5689,.F.);
#8262=ORIENTED_EDGE('',*,*,#5692,.F.);
#8263=ORIENTED_EDGE('',*,*,#5695,.F.);
#8264=ORIENTED_EDGE('',*,*,#5698,.F.);
#8265=ORIENTED_EDGE('',*,*,#5701,.F.);
#8266=ORIENTED_EDGE('',*,*,#5704,.F.);
#8267=ORIENTED_EDGE('',*,*,#5707,.F.);
#8268=ORIENTED_EDGE('',*,*,#5710,.F.);
#8269=ORIENTED_EDGE('',*,*,#5718,.F.);
#8270=ORIENTED_EDGE('',*,*,#5719,.F.);
#8271=ORIENTED_EDGE('',*,*,#5615,.F.);
#8272=ORIENTED_EDGE('',*,*,#5619,.F.);
#8273=ORIENTED_EDGE('',*,*,#5622,.F.);
#8274=ORIENTED_EDGE('',*,*,#5625,.F.);
#8275=ORIENTED_EDGE('',*,*,#5628,.F.);
#8276=ORIENTED_EDGE('',*,*,#5631,.F.);
#8277=ORIENTED_EDGE('',*,*,#5634,.F.);
#8278=ORIENTED_EDGE('',*,*,#5637,.F.);
#8279=ORIENTED_EDGE('',*,*,#5640,.F.);
#8280=ORIENTED_EDGE('',*,*,#5643,.F.);
#8281=ORIENTED_EDGE('',*,*,#5646,.F.);
#8282=ORIENTED_EDGE('',*,*,#5649,.F.);
#8283=ORIENTED_EDGE('',*,*,#5652,.F.);
#8284=ORIENTED_EDGE('',*,*,#5655,.F.);
#8285=ORIENTED_EDGE('',*,*,#5658,.F.);
#8286=ORIENTED_EDGE('',*,*,#5661,.F.);
#8287=ORIENTED_EDGE('',*,*,#5720,.F.);
#8288=ORIENTED_EDGE('',*,*,#5709,.T.);
#8289=ORIENTED_EDGE('',*,*,#5721,.F.);
#8290=ORIENTED_EDGE('',*,*,#5722,.F.);
#8291=ORIENTED_EDGE('',*,*,#5718,.T.);
#8292=ORIENTED_EDGE('',*,*,#5712,.T.);
#8293=ORIENTED_EDGE('',*,*,#5715,.T.);
#8294=ORIENTED_EDGE('',*,*,#5723,.F.);
#8295=ORIENTED_EDGE('',*,*,#5662,.F.);
#8296=ORIENTED_EDGE('',*,*,#5659,.F.);
#8297=ORIENTED_EDGE('',*,*,#5656,.F.);
#8298=ORIENTED_EDGE('',*,*,#5653,.F.);
#8299=ORIENTED_EDGE('',*,*,#5650,.F.);
#8300=ORIENTED_EDGE('',*,*,#5647,.F.);
#8301=ORIENTED_EDGE('',*,*,#5644,.F.);
#8302=ORIENTED_EDGE('',*,*,#5641,.F.);
#8303=ORIENTED_EDGE('',*,*,#5638,.F.);
#8304=ORIENTED_EDGE('',*,*,#5635,.F.);
#8305=ORIENTED_EDGE('',*,*,#5632,.F.);
#8306=ORIENTED_EDGE('',*,*,#5629,.F.);
#8307=ORIENTED_EDGE('',*,*,#5626,.F.);
#8308=ORIENTED_EDGE('',*,*,#5623,.F.);
#8309=ORIENTED_EDGE('',*,*,#5620,.F.);
#8310=ORIENTED_EDGE('',*,*,#5617,.F.);
#8311=ORIENTED_EDGE('',*,*,#5724,.F.);
#8312=ORIENTED_EDGE('',*,*,#5721,.T.);
#8313=ORIENTED_EDGE('',*,*,#5711,.T.);
#8314=ORIENTED_EDGE('',*,*,#5708,.T.);
#8315=ORIENTED_EDGE('',*,*,#5705,.T.);
#8316=ORIENTED_EDGE('',*,*,#5702,.T.);
#8317=ORIENTED_EDGE('',*,*,#5699,.T.);
#8318=ORIENTED_EDGE('',*,*,#5696,.T.);
#8319=ORIENTED_EDGE('',*,*,#5693,.T.);
#8320=ORIENTED_EDGE('',*,*,#5690,.T.);
#8321=ORIENTED_EDGE('',*,*,#5687,.T.);
#8322=ORIENTED_EDGE('',*,*,#5684,.T.);
#8323=ORIENTED_EDGE('',*,*,#5681,.T.);
#8324=ORIENTED_EDGE('',*,*,#5678,.T.);
#8325=ORIENTED_EDGE('',*,*,#5675,.T.);
#8326=ORIENTED_EDGE('',*,*,#5672,.T.);
#8327=ORIENTED_EDGE('',*,*,#5669,.T.);
#8328=ORIENTED_EDGE('',*,*,#5666,.T.);
#8329=ORIENTED_EDGE('',*,*,#5660,.T.);
#8330=ORIENTED_EDGE('',*,*,#5723,.T.);
#8331=ORIENTED_EDGE('',*,*,#5714,.T.);
#8332=ORIENTED_EDGE('',*,*,#5720,.T.);
#8333=ORIENTED_EDGE('',*,*,#5725,.F.);
#8334=ORIENTED_EDGE('',*,*,#5726,.T.);
#8335=ORIENTED_EDGE('',*,*,#5727,.T.);
#8336=ORIENTED_EDGE('',*,*,#5728,.F.);
#8337=ORIENTED_EDGE('',*,*,#5729,.F.);
#8338=ORIENTED_EDGE('',*,*,#5730,.T.);
#8339=ORIENTED_EDGE('',*,*,#5731,.T.);
#8340=ORIENTED_EDGE('',*,*,#5726,.F.);
#8341=ORIENTED_EDGE('',*,*,#5732,.F.);
#8342=ORIENTED_EDGE('',*,*,#5733,.T.);
#8343=ORIENTED_EDGE('',*,*,#5734,.T.);
#8344=ORIENTED_EDGE('',*,*,#5730,.F.);
#8345=ORIENTED_EDGE('',*,*,#5735,.F.);
#8346=ORIENTED_EDGE('',*,*,#5736,.T.);
#8347=ORIENTED_EDGE('',*,*,#5737,.T.);
#8348=ORIENTED_EDGE('',*,*,#5733,.F.);
#8349=ORIENTED_EDGE('',*,*,#5738,.F.);
#8350=ORIENTED_EDGE('',*,*,#5739,.T.);
#8351=ORIENTED_EDGE('',*,*,#5740,.T.);
#8352=ORIENTED_EDGE('',*,*,#5736,.F.);
#8353=ORIENTED_EDGE('',*,*,#5741,.F.);
#8354=ORIENTED_EDGE('',*,*,#5728,.T.);
#8355=ORIENTED_EDGE('',*,*,#5742,.T.);
#8356=ORIENTED_EDGE('',*,*,#5739,.F.);
#8357=ORIENTED_EDGE('',*,*,#5742,.F.);
#8358=ORIENTED_EDGE('',*,*,#5727,.F.);
#8359=ORIENTED_EDGE('',*,*,#5731,.F.);
#8360=ORIENTED_EDGE('',*,*,#5734,.F.);
#8361=ORIENTED_EDGE('',*,*,#5737,.F.);
#8362=ORIENTED_EDGE('',*,*,#5740,.F.);
#8363=ORIENTED_EDGE('',*,*,#5743,.T.);
#8364=ORIENTED_EDGE('',*,*,#5719,.T.);
#8365=ORIENTED_EDGE('',*,*,#5722,.T.);
#8366=ORIENTED_EDGE('',*,*,#5724,.T.);
#8367=ORIENTED_EDGE('',*,*,#5616,.F.);
#8368=ORIENTED_EDGE('',*,*,#5743,.F.);
#8369=ORIENTED_EDGE('',*,*,#5744,.T.);
#8370=ORIENTED_EDGE('',*,*,#5745,.T.);
#8371=ORIENTED_EDGE('',*,*,#5744,.F.);
#8372=ORIENTED_EDGE('',*,*,#5745,.F.);
#8373=ORIENTED_EDGE('',*,*,#5725,.T.);
#8374=ORIENTED_EDGE('',*,*,#5741,.T.);
#8375=ORIENTED_EDGE('',*,*,#5738,.T.);
#8376=ORIENTED_EDGE('',*,*,#5735,.T.);
#8377=ORIENTED_EDGE('',*,*,#5732,.T.);
#8378=ORIENTED_EDGE('',*,*,#5729,.T.);
#8379=ORIENTED_EDGE('',*,*,#5717,.T.);
#9132=CYLINDRICAL_SURFACE('',#10506,0.1954);
#9133=CYLINDRICAL_SURFACE('',#10508,0.1954);
#9134=CYLINDRICAL_SURFACE('',#10509,0.1954);
#9135=CYLINDRICAL_SURFACE('',#10510,0.1954);
#9136=CYLINDRICAL_SURFACE('',#10511,0.1954);
#9137=CYLINDRICAL_SURFACE('',#10512,0.1954);
#9138=CYLINDRICAL_SURFACE('',#10513,0.1954);
#9139=CYLINDRICAL_SURFACE('',#10514,0.1954);
#9140=CYLINDRICAL_SURFACE('',#10515,0.1954);
#9141=CYLINDRICAL_SURFACE('',#10516,0.1954);
#9142=CYLINDRICAL_SURFACE('',#10517,0.1954);
#9143=CYLINDRICAL_SURFACE('',#10518,0.1954);
#9144=CYLINDRICAL_SURFACE('',#10519,0.1954);
#9145=CYLINDRICAL_SURFACE('',#10520,0.1954);
#9146=CYLINDRICAL_SURFACE('',#10521,0.1954);
#9147=CYLINDRICAL_SURFACE('',#10522,0.1954);
#9148=CYLINDRICAL_SURFACE('',#10523,0.15555);
#9149=CYLINDRICAL_SURFACE('',#10525,0.15555);
#9150=CYLINDRICAL_SURFACE('',#10526,0.15555);
#9151=CYLINDRICAL_SURFACE('',#10527,0.15555);
#9152=CYLINDRICAL_SURFACE('',#10528,0.15555);
#9153=CYLINDRICAL_SURFACE('',#10529,0.15555);
#9154=CYLINDRICAL_SURFACE('',#10530,0.15555);
#9155=CYLINDRICAL_SURFACE('',#10531,0.15555);
#9156=CYLINDRICAL_SURFACE('',#10532,0.15555);
#9157=CYLINDRICAL_SURFACE('',#10533,0.15555);
#9158=CYLINDRICAL_SURFACE('',#10534,0.15555);
#9159=CYLINDRICAL_SURFACE('',#10535,0.15555);
#9160=CYLINDRICAL_SURFACE('',#10536,0.15555);
#9161=CYLINDRICAL_SURFACE('',#10537,0.15555);
#9162=CYLINDRICAL_SURFACE('',#10538,0.15555);
#9163=CYLINDRICAL_SURFACE('',#10539,0.15555);
#9164=CYLINDRICAL_SURFACE('',#10543,0.15555);
#9165=CYLINDRICAL_SURFACE('',#10545,0.1954);
#9166=CYLINDRICAL_SURFACE('',#10555,0.35);
#9631=ADVANCED_FACE('',(#841),#9132,.T.);
#9632=ADVANCED_FACE('',(#842),#9133,.T.);
#9633=ADVANCED_FACE('',(#843),#9134,.T.);
#9634=ADVANCED_FACE('',(#844),#9135,.T.);
#9635=ADVANCED_FACE('',(#845),#9136,.T.);
#9636=ADVANCED_FACE('',(#846),#9137,.T.);
#9637=ADVANCED_FACE('',(#847),#9138,.T.);
#9638=ADVANCED_FACE('',(#848),#9139,.T.);
#9639=ADVANCED_FACE('',(#849),#9140,.T.);
#9640=ADVANCED_FACE('',(#850),#9141,.T.);
#9641=ADVANCED_FACE('',(#851),#9142,.T.);
#9642=ADVANCED_FACE('',(#852),#9143,.T.);
#9643=ADVANCED_FACE('',(#853),#9144,.T.);
#9644=ADVANCED_FACE('',(#854),#9145,.T.);
#9645=ADVANCED_FACE('',(#855),#9146,.T.);
#9646=ADVANCED_FACE('',(#856),#9147,.T.);
#9647=ADVANCED_FACE('',(#857),#9148,.T.);
#9648=ADVANCED_FACE('',(#858),#9149,.T.);
#9649=ADVANCED_FACE('',(#859),#9150,.T.);
#9650=ADVANCED_FACE('',(#860),#9151,.T.);
#9651=ADVANCED_FACE('',(#861),#9152,.T.);
#9652=ADVANCED_FACE('',(#862),#9153,.T.);
#9653=ADVANCED_FACE('',(#863),#9154,.T.);
#9654=ADVANCED_FACE('',(#864),#9155,.T.);
#9655=ADVANCED_FACE('',(#865),#9156,.T.);
#9656=ADVANCED_FACE('',(#866),#9157,.T.);
#9657=ADVANCED_FACE('',(#867),#9158,.T.);
#9658=ADVANCED_FACE('',(#868),#9159,.T.);
#9659=ADVANCED_FACE('',(#869),#9160,.T.);
#9660=ADVANCED_FACE('',(#870),#9161,.T.);
#9661=ADVANCED_FACE('',(#871),#9162,.T.);
#9662=ADVANCED_FACE('',(#872),#9163,.T.);
#9663=ADVANCED_FACE('',(#873),#139,.T.);
#9664=ADVANCED_FACE('',(#874),#229,.F.);
#9665=ADVANCED_FACE('',(#875),#9164,.T.);
#9666=ADVANCED_FACE('',(#876),#230,.F.);
#9667=ADVANCED_FACE('',(#877),#9165,.T.);
#9668=ADVANCED_FACE('',(#878),#409,.F.);
#9669=ADVANCED_FACE('',(#879),#410,.F.);
#9670=ADVANCED_FACE('',(#880),#411,.F.);
#9671=ADVANCED_FACE('',(#881),#412,.F.);
#9672=ADVANCED_FACE('',(#882),#413,.F.);
#9673=ADVANCED_FACE('',(#883),#414,.F.);
#9674=ADVANCED_FACE('',(#884),#415,.F.);
#9675=ADVANCED_FACE('',(#885,#296),#416,.T.);
#9676=ADVANCED_FACE('',(#886),#9166,.T.);
#9677=ADVANCED_FACE('',(#887,#297),#417,.F.);
#9678=ADVANCED_FACE('',(#888),#418,.T.);
#9781=CLOSED_SHELL('',(#9631,#9632,#9633,#9634,#9635,#9636,#9637,#9638,
#9639,#9640,#9641,#9642,#9643,#9644,#9645,#9646,#9647,#9648,#9649,#9650,
#9651,#9652,#9653,#9654,#9655,#9656,#9657,#9658,#9659,#9660,#9661,#9662,
#9663,#9664,#9665,#9666,#9667,#9668,#9669,#9670,#9671,#9672,#9673,#9674,
#9675,#9676,#9677,#9678));
#10505=AXIS2_PLACEMENT_3D('',#29655,#12182,#12183);
#10506=AXIS2_PLACEMENT_3D('',#29656,#12184,#12185);
#10507=AXIS2_PLACEMENT_3D('',#29672,#12187,#12188);
#10508=AXIS2_PLACEMENT_3D('',#29680,#12189,#12190);
#10509=AXIS2_PLACEMENT_3D('',#29728,#12192,#12193);
#10510=AXIS2_PLACEMENT_3D('',#29776,#12195,#12196);
#10511=AXIS2_PLACEMENT_3D('',#29824,#12198,#12199);
#10512=AXIS2_PLACEMENT_3D('',#29872,#12201,#12202);
#10513=AXIS2_PLACEMENT_3D('',#29920,#12204,#12205);
#10514=AXIS2_PLACEMENT_3D('',#29968,#12207,#12208);
#10515=AXIS2_PLACEMENT_3D('',#30022,#12210,#12211);
#10516=AXIS2_PLACEMENT_3D('',#30070,#12213,#12214);
#10517=AXIS2_PLACEMENT_3D('',#30118,#12216,#12217);
#10518=AXIS2_PLACEMENT_3D('',#30172,#12219,#12220);
#10519=AXIS2_PLACEMENT_3D('',#30220,#12222,#12223);
#10520=AXIS2_PLACEMENT_3D('',#30268,#12225,#12226);
#10521=AXIS2_PLACEMENT_3D('',#30316,#12228,#12229);
#10522=AXIS2_PLACEMENT_3D('',#30367,#12231,#12232);
#10523=AXIS2_PLACEMENT_3D('',#30415,#12234,#12235);
#10524=AXIS2_PLACEMENT_3D('',#30429,#12237,#12238);
#10525=AXIS2_PLACEMENT_3D('',#30437,#12239,#12240);
#10526=AXIS2_PLACEMENT_3D('',#30461,#12242,#12243);
#10527=AXIS2_PLACEMENT_3D('',#30485,#12245,#12246);
#10528=AXIS2_PLACEMENT_3D('',#30511,#12248,#12249);
#10529=AXIS2_PLACEMENT_3D('',#30535,#12251,#12252);
#10530=AXIS2_PLACEMENT_3D('',#30559,#12254,#12255);
#10531=AXIS2_PLACEMENT_3D('',#30584,#12257,#12258);
#10532=AXIS2_PLACEMENT_3D('',#30609,#12260,#12261);
#10533=AXIS2_PLACEMENT_3D('',#30633,#12263,#12264);
#10534=AXIS2_PLACEMENT_3D('',#30658,#12266,#12267);
#10535=AXIS2_PLACEMENT_3D('',#30683,#12269,#12270);
#10536=AXIS2_PLACEMENT_3D('',#30707,#12272,#12273);
#10537=AXIS2_PLACEMENT_3D('',#30731,#12275,#12276);
#10538=AXIS2_PLACEMENT_3D('',#30756,#12278,#12279);
#10539=AXIS2_PLACEMENT_3D('',#30781,#12281,#12282);
#10540=AXIS2_PLACEMENT_3D('',#30805,#12284,#12285);
#10541=AXIS2_PLACEMENT_3D('',#30922,#12286,#12287);
#10542=AXIS2_PLACEMENT_3D('',#30989,#12289,#12290);
#10543=AXIS2_PLACEMENT_3D('',#31494,#12291,#12292);
#10544=AXIS2_PLACEMENT_3D('',#31505,#12293,#12294);
#10545=AXIS2_PLACEMENT_3D('',#32006,#12295,#12296);
#10546=AXIS2_PLACEMENT_3D('',#32007,#12297,#12298);
#10547=AXIS2_PLACEMENT_3D('',#32016,#12303,#12304);
#10548=AXIS2_PLACEMENT_3D('',#32022,#12308,#12309);
#10549=AXIS2_PLACEMENT_3D('',#32028,#12313,#12314);
#10550=AXIS2_PLACEMENT_3D('',#32034,#12318,#12319);
#10551=AXIS2_PLACEMENT_3D('',#32040,#12323,#12324);
#10552=AXIS2_PLACEMENT_3D('',#32043,#12327,#12328);
#10553=AXIS2_PLACEMENT_3D('',#32044,#12329,#12330);
#10554=AXIS2_PLACEMENT_3D('',#32046,#12331,#12332);
#10555=AXIS2_PLACEMENT_3D('',#32047,#12333,#12334);
#10556=AXIS2_PLACEMENT_3D('',#32050,#12336,#12337);
#10557=AXIS2_PLACEMENT_3D('',#32051,#12338,#12339);
#10558=AXIS2_PLACEMENT_3D('',#32052,#12340,#12341);
#12182=DIRECTION('axis',(0.,0.,1.));
#12183=DIRECTION('refdir',(1.,0.,0.));
#12184=DIRECTION('center_axis',(0.,0.,1.));
#12185=DIRECTION('ref_axis',(1.,0.,0.));
#12186=DIRECTION('',(0.,0.,-1.));
#12187=DIRECTION('center_axis',(0.,0.,-1.));
#12188=DIRECTION('ref_axis',(1.,0.,0.));
#12189=DIRECTION('center_axis',(0.,0.,1.));
#12190=DIRECTION('ref_axis',(1.,0.,0.));
#12191=DIRECTION('',(0.,0.,-1.));
#12192=DIRECTION('center_axis',(0.,0.,1.));
#12193=DIRECTION('ref_axis',(1.,0.,0.));
#12194=DIRECTION('',(0.,0.,-1.));
#12195=DIRECTION('center_axis',(0.,0.,1.));
#12196=DIRECTION('ref_axis',(1.,0.,0.));
#12197=DIRECTION('',(0.,0.,-1.));
#12198=DIRECTION('center_axis',(0.,0.,1.));
#12199=DIRECTION('ref_axis',(1.,0.,0.));
#12200=DIRECTION('',(0.,0.,-1.));
#12201=DIRECTION('center_axis',(0.,0.,1.));
#12202=DIRECTION('ref_axis',(1.,0.,0.));
#12203=DIRECTION('',(0.,0.,-1.));
#12204=DIRECTION('center_axis',(0.,0.,1.));
#12205=DIRECTION('ref_axis',(1.,0.,0.));
#12206=DIRECTION('',(0.,0.,-1.));
#12207=DIRECTION('center_axis',(0.,0.,1.));
#12208=DIRECTION('ref_axis',(1.,0.,0.));
#12209=DIRECTION('',(0.,0.,-1.));
#12210=DIRECTION('center_axis',(0.,0.,1.));
#12211=DIRECTION('ref_axis',(1.,0.,0.));
#12212=DIRECTION('',(0.,0.,-1.));
#12213=DIRECTION('center_axis',(0.,0.,1.));
#12214=DIRECTION('ref_axis',(1.,0.,0.));
#12215=DIRECTION('',(0.,0.,-1.));
#12216=DIRECTION('center_axis',(0.,0.,1.));
#12217=DIRECTION('ref_axis',(1.,0.,0.));
#12218=DIRECTION('',(0.,0.,-1.));
#12219=DIRECTION('center_axis',(0.,0.,1.));
#12220=DIRECTION('ref_axis',(1.,0.,0.));
#12221=DIRECTION('',(0.,0.,-1.));
#12222=DIRECTION('center_axis',(0.,0.,1.));
#12223=DIRECTION('ref_axis',(1.,0.,0.));
#12224=DIRECTION('',(0.,0.,-1.));
#12225=DIRECTION('center_axis',(0.,0.,1.));
#12226=DIRECTION('ref_axis',(1.,0.,0.));
#12227=DIRECTION('',(0.,0.,-1.));
#12228=DIRECTION('center_axis',(0.,0.,1.));
#12229=DIRECTION('ref_axis',(1.,0.,0.));
#12230=DIRECTION('',(0.,0.,-1.));
#12231=DIRECTION('center_axis',(0.,0.,1.));
#12232=DIRECTION('ref_axis',(1.,0.,0.));
#12233=DIRECTION('',(0.,0.,-1.));
#12234=DIRECTION('center_axis',(0.,0.,1.));
#12235=DIRECTION('ref_axis',(1.,1.29731060939901E-13,0.));
#12236=DIRECTION('',(0.,0.,1.));
#12237=DIRECTION('center_axis',(0.,0.,-1.));
#12238=DIRECTION('ref_axis',(1.,1.29731060939901E-13,0.));
#12239=DIRECTION('center_axis',(0.,0.,1.));
#12240=DIRECTION('ref_axis',(1.,1.29731060939901E-13,0.));
#12241=DIRECTION('',(0.,0.,1.));
#12242=DIRECTION('center_axis',(0.,0.,1.));
#12243=DIRECTION('ref_axis',(1.,1.29731060939901E-13,0.));
#12244=DIRECTION('',(0.,0.,1.));
#12245=DIRECTION('center_axis',(0.,0.,1.));
#12246=DIRECTION('ref_axis',(1.,1.29731060939901E-13,0.));
#12247=DIRECTION('',(0.,0.,1.));
#12248=DIRECTION('center_axis',(0.,0.,1.));
#12249=DIRECTION('ref_axis',(1.,1.29731060939901E-13,0.));
#12250=DIRECTION('',(0.,0.,1.));
#12251=DIRECTION('center_axis',(0.,0.,1.));
#12252=DIRECTION('ref_axis',(1.,1.29731060939901E-13,0.));
#12253=DIRECTION('',(0.,0.,1.));
#12254=DIRECTION('center_axis',(0.,0.,1.));
#12255=DIRECTION('ref_axis',(1.,1.29731060939901E-13,0.));
#12256=DIRECTION('',(0.,0.,1.));
#12257=DIRECTION('center_axis',(0.,0.,1.));
#12258=DIRECTION('ref_axis',(1.,1.29731060939901E-13,0.));
#12259=DIRECTION('',(0.,0.,1.));
#12260=DIRECTION('center_axis',(0.,0.,1.));
#12261=DIRECTION('ref_axis',(1.,1.29731060939901E-13,0.));
#12262=DIRECTION('',(0.,0.,1.));
#12263=DIRECTION('center_axis',(0.,0.,1.));
#12264=DIRECTION('ref_axis',(1.,1.29731060939901E-13,0.));
#12265=DIRECTION('',(0.,0.,1.));
#12266=DIRECTION('center_axis',(0.,0.,1.));
#12267=DIRECTION('ref_axis',(1.,1.29731060939901E-13,0.));
#12268=DIRECTION('',(0.,0.,1.));
#12269=DIRECTION('center_axis',(0.,0.,1.));
#12270=DIRECTION('ref_axis',(1.,1.29731060939901E-13,0.));
#12271=DIRECTION('',(0.,0.,1.));
#12272=DIRECTION('center_axis',(0.,0.,1.));
#12273=DIRECTION('ref_axis',(1.,1.29731060939901E-13,0.));
#12274=DIRECTION('',(0.,0.,1.));
#12275=DIRECTION('center_axis',(0.,0.,1.));
#12276=DIRECTION('ref_axis',(1.,1.29731060939901E-13,0.));
#12277=DIRECTION('',(0.,0.,1.));
#12278=DIRECTION('center_axis',(0.,0.,1.));
#12279=DIRECTION('ref_axis',(1.,1.29731060939901E-13,0.));
#12280=DIRECTION('',(0.,0.,1.));
#12281=DIRECTION('center_axis',(0.,0.,1.));
#12282=DIRECTION('ref_axis',(1.,1.29731060939901E-13,0.));
#12283=DIRECTION('',(0.,0.,1.));
#12284=DIRECTION('center_axis',(0.,0.,-1.));
#12285=DIRECTION('ref_axis',(1.,0.,0.));
#12286=DIRECTION('center_axis',(0.,0.,-1.));
#12287=DIRECTION('ref_axis',(1.,0.,0.));
#12288=DIRECTION('',(0.707106781186548,8.65956056235494E-17,0.707106781186547));
#12289=DIRECTION('center_axis',(0.,0.,1.));
#12290=DIRECTION('ref_axis',(1.,0.,0.));
#12291=DIRECTION('center_axis',(0.,0.,1.));
#12292=DIRECTION('ref_axis',(1.,1.29731060939901E-13,0.));
#12293=DIRECTION('center_axis',(0.,0.,-1.));
#12294=DIRECTION('ref_axis',(1.,1.29731060939901E-13,0.));
#12295=DIRECTION('center_axis',(0.,0.,1.));
#12296=DIRECTION('ref_axis',(1.,0.,0.));
#12297=DIRECTION('center_axis',(-1.60246890531964E-16,-1.,0.));
#12298=DIRECTION('ref_axis',(1.,-1.60246890531964E-16,0.));
#12299=DIRECTION('',(1.,-1.60246890531964E-16,0.));
#12300=DIRECTION('',(0.,0.,1.));
#12301=DIRECTION('',(1.,-1.60246890531964E-16,0.));
#12302=DIRECTION('',(0.,0.,1.));
#12303=DIRECTION('center_axis',(-0.866025403784439,-0.5,0.));
#12304=DIRECTION('ref_axis',(0.5,-0.866025403784439,0.));
#12305=DIRECTION('',(0.5,-0.866025403784439,0.));
#12306=DIRECTION('',(0.,0.,1.));
#12307=DIRECTION('',(0.5,-0.866025403784439,0.));
#12308=DIRECTION('center_axis',(-0.866025403784439,0.5,0.));
#12309=DIRECTION('ref_axis',(-0.5,-0.866025403784439,0.));
#12310=DIRECTION('',(-0.5,-0.866025403784439,0.));
#12311=DIRECTION('',(0.,0.,1.));
#12312=DIRECTION('',(-0.5,-0.866025403784439,0.));
#12313=DIRECTION('center_axis',(1.60246890531964E-16,1.,0.));
#12314=DIRECTION('ref_axis',(-1.,1.60246890531964E-16,0.));
#12315=DIRECTION('',(-1.,1.60246890531964E-16,0.));
#12316=DIRECTION('',(0.,0.,1.));
#12317=DIRECTION('',(-1.,1.60246890531964E-16,0.));
#12318=DIRECTION('center_axis',(0.866025403784439,0.5,0.));
#12319=DIRECTION('ref_axis',(-0.5,0.866025403784439,0.));
#12320=DIRECTION('',(-0.5,0.866025403784439,0.));
#12321=DIRECTION('',(0.,0.,1.));
#12322=DIRECTION('',(-0.5,0.866025403784439,0.));
#12323=DIRECTION('center_axis',(0.866025403784439,-0.5,0.));
#12324=DIRECTION('ref_axis',(0.5,0.866025403784439,0.));
#12325=DIRECTION('',(0.5,0.866025403784439,0.));
#12326=DIRECTION('',(0.5,0.866025403784439,0.));
#12327=DIRECTION('center_axis',(0.,0.,1.));
#12328=DIRECTION('ref_axis',(1.,0.,0.));
#12329=DIRECTION('center_axis',(0.,0.,1.));
#12330=DIRECTION('ref_axis',(1.,0.,0.));
#12331=DIRECTION('center_axis',(0.,0.,1.));
#12332=DIRECTION('ref_axis',(1.,0.,0.));
#12333=DIRECTION('center_axis',(0.,0.,1.));
#12334=DIRECTION('ref_axis',(1.,0.,0.));
#12335=DIRECTION('',(0.,0.,-1.));
#12336=DIRECTION('center_axis',(0.,0.,1.));
#12337=DIRECTION('ref_axis',(1.,0.,0.));
#12338=DIRECTION('center_axis',(0.,0.,1.));
#12339=DIRECTION('ref_axis',(1.,0.,0.));
#12340=DIRECTION('center_axis',(0.,0.,1.));
#12341=DIRECTION('ref_axis',(1.,0.,0.));
#29655=CARTESIAN_POINT('',(0.,0.,0.));
#29656=CARTESIAN_POINT('Origin',(0.,0.,0.));
#29657=CARTESIAN_POINT('',(-0.195633559071744,0.00012731057411345,0.0225869692124231));
#29658=CARTESIAN_POINT('',(-0.195587799559821,0.000207186393275607,0.0124130307875758));
#29659=CARTESIAN_POINT('',(-0.1954,-2.39295984553393E-17,0.));
#29660=CARTESIAN_POINT('',(0.0861525859670522,0.175382131162755,0.));
#29661=CARTESIAN_POINT('Ctrl Pts',(-0.195633559071744,0.00012731057411345,
0.0225869692124231));
#29662=CARTESIAN_POINT('Ctrl Pts',(-0.195680032440099,0.00682557629313676,
0.0222037301306047));
#29663=CARTESIAN_POINT('Ctrl Pts',(-0.195365903766855,0.0135191473590706,
0.0218204910487863));
#29664=CARTESIAN_POINT('Ctrl Pts',(-0.194676806606145,0.0201735328972743,
0.0214372519669679));
#29665=CARTESIAN_POINT('Ctrl Pts',(-0.188017193281744,0.0844832371344698,
0.01773353028412));
#29666=CARTESIAN_POINT('Ctrl Pts',(-0.146336311091822,0.145133095416213,
0.0140298086012721));
#29667=CARTESIAN_POINT('Ctrl Pts',(-0.0886884671668765,0.17445317403525,
0.0103260869184242));
#29668=CARTESIAN_POINT('Ctrl Pts',(-0.0351138290053491,0.201701592986141,
0.00688405794561611));
#29669=CARTESIAN_POINT('Ctrl Pts',(0.0322511385444639,0.201891139473935,
0.00344202897280807));
#29670=CARTESIAN_POINT('Ctrl Pts',(0.0863567639152679,0.175641488315944,
2.92734586571086E-18));
#29671=CARTESIAN_POINT('',(-0.0861525859670574,0.175382131162752,1.38777878078145E-17));
#29672=CARTESIAN_POINT('Origin',(0.,0.,0.));
#29673=CARTESIAN_POINT('Ctrl Pts',(-0.0861525859670571,0.175382131162752,
2.28983498828939E-16));
#29674=CARTESIAN_POINT('Ctrl Pts',(-0.144496782441851,0.146721837385109,
0.00370621399437224));
#29675=CARTESIAN_POINT('Ctrl Pts',(-0.18691020329229,0.0869083656944534,
0.00741242798874424));
#29676=CARTESIAN_POINT('Ctrl Pts',(-0.194380023116171,0.0227435527544788,
0.0111186419831163));
#29677=CARTESIAN_POINT('Ctrl Pts',(-0.195249630318745,0.0152737362394887,
0.0115501049179361));
#29678=CARTESIAN_POINT('Ctrl Pts',(-0.195645657185248,0.00774494727773659,
0.0119815678527559));
#29679=CARTESIAN_POINT('Ctrl Pts',(-0.195587799559821,0.000207186393275607,
0.0124130307875758));
#29680=CARTESIAN_POINT('Origin',(0.,0.,0.));
#29681=CARTESIAN_POINT('',(-0.195128203910989,9.79727872364722E-5,0.092586969212423));
#29682=CARTESIAN_POINT('',(-0.195118672945361,9.16100096969453E-5,0.0824130307875757));
#29683=CARTESIAN_POINT('',(-0.1954,-2.39295984553393E-17,0.));
#29684=CARTESIAN_POINT('Ctrl Pts',(-0.195128203910989,9.79727872364722E-5,
0.092586969212423));
#29685=CARTESIAN_POINT('Ctrl Pts',(-0.19524730612105,0.0263901717292074,
0.0910927268943587));
#29686=CARTESIAN_POINT('Ctrl Pts',(-0.190305141123492,0.0526394079969068,
0.0895984845762944));
#29687=CARTESIAN_POINT('Ctrl Pts',(-0.180089049647467,0.0766440059940591,
0.0881042422582301));
#29688=CARTESIAN_POINT('Ctrl Pts',(-0.154766811710363,0.136143291361155,
0.0844005205753822));
#29689=CARTESIAN_POINT('Ctrl Pts',(-0.0970428066964404,0.181852045762203,
0.0806967988925343));
#29690=CARTESIAN_POINT('Ctrl Pts',(-0.0333230591869142,0.192861999489257,
0.0769930772096863));
#29691=CARTESIAN_POINT('Ctrl Pts',(0.030396688322612,0.20387195321631,0.0732893555268384));
#29692=CARTESIAN_POINT('Ctrl Pts',(0.100112178327742,0.18018310626937,0.0695856338439906));
#29693=CARTESIAN_POINT('Ctrl Pts',(0.143930998255098,0.132629143144902,
0.0658819121611426));
#29694=CARTESIAN_POINT('Ctrl Pts',(0.187749818182454,0.0850751800204342,
0.0621781904782947));
#29695=CARTESIAN_POINT('Ctrl Pts',(0.205671968032037,0.0136561007184397,
0.0584744687954468));
#29696=CARTESIAN_POINT('Ctrl Pts',(0.189499805994521,-0.0489512382298273,
0.0547707471125989));
#29697=CARTESIAN_POINT('Ctrl Pts',(0.173327643957006,-0.111558577178094,
0.051067025429751));
#29698=CARTESIAN_POINT('Ctrl Pts',(0.123061170032392,-0.165354175772633,
0.0473633037469032));
#29699=CARTESIAN_POINT('Ctrl Pts',(0.0616932989107385,-0.18573955796291,
0.0436595820640553));
#29700=CARTESIAN_POINT('Ctrl Pts',(0.000325427789084558,-0.206124940153187,
0.0399558603812074));
#29701=CARTESIAN_POINT('Ctrl Pts',(-0.0721438405296094,-0.193100105939202,
0.0362521386983595));
#29702=CARTESIAN_POINT('Ctrl Pts',(-0.122559302459517,-0.152602913735885,
0.0325484170155115));
#29703=CARTESIAN_POINT('Ctrl Pts',(-0.167758072371516,-0.11629613001496,
0.029227934414482));
#29704=CARTESIAN_POINT('Ctrl Pts',(-0.195230901779331,-0.0579081973692791,
0.0259074518134526));
#29705=CARTESIAN_POINT('Ctrl Pts',(-0.195633559071744,0.00012731057411345,
0.0225869692124231));
#29706=CARTESIAN_POINT('Ctrl Pts',(-0.195587799559821,0.000207186393275607,
0.0124130307875758));
#29707=CARTESIAN_POINT('Ctrl Pts',(-0.195148667238412,-0.0570034995103637,
0.015687781847128));
#29708=CARTESIAN_POINT('Ctrl Pts',(-0.168562951923343,-0.114731024226281,
0.0189625329066803));
#29709=CARTESIAN_POINT('Ctrl Pts',(-0.12444215732779,-0.151113938431406,
0.0222372839662326));
#29710=CARTESIAN_POINT('Ctrl Pts',(-0.0745082529182101,-0.192290462488019,
0.0259434979606046));
#29711=CARTESIAN_POINT('Ctrl Pts',(-0.00211422530173012,-0.20612735641195,
0.0296497119549767));
#29712=CARTESIAN_POINT('Ctrl Pts',(0.0595334795120667,-0.186428772433344,
0.0333559259493488));
#29713=CARTESIAN_POINT('Ctrl Pts',(0.121181184325864,-0.166730188454737,
0.0370621399437209));
#29714=CARTESIAN_POINT('Ctrl Pts',(0.172082566336977,-0.113496126573593,
0.040768353938093));
#29715=CARTESIAN_POINT('Ctrl Pts',(0.18894870924304,-0.0510370283185346,
0.0444745679324651));
#29716=CARTESIAN_POINT('Ctrl Pts',(0.205814852149104,0.0114220699365238,
0.0481807819268372));
#29717=CARTESIAN_POINT('Ctrl Pts',(0.188645755950116,0.0831062045654966,
0.0518869959212093));
#29718=CARTESIAN_POINT('Ctrl Pts',(0.145292142815886,0.131145007703775,
0.0555932099155814));
#29719=CARTESIAN_POINT('Ctrl Pts',(0.101938529681656,0.179183810842053,
0.0592994239099535));
#29720=CARTESIAN_POINT('Ctrl Pts',(0.0324003996121834,0.203577282489637,
0.0630056379043256));
#29721=CARTESIAN_POINT('Ctrl Pts',(-0.0314654015224673,0.193172336479658,
0.0667118518986976));
#29722=CARTESIAN_POINT('Ctrl Pts',(-0.0953312026571179,0.18276739046968,
0.0704180658930697));
#29723=CARTESIAN_POINT('Ctrl Pts',(-0.153524674856946,0.137564026802139,
0.0741242798874417));
#29724=CARTESIAN_POINT('Ctrl Pts',(-0.179395555636014,0.0782560471576942,
0.0778304938818138));
#29725=CARTESIAN_POINT('Ctrl Pts',(-0.190058212652462,0.0538123240897563,
0.0793580061837345));
#29726=CARTESIAN_POINT('Ctrl Pts',(-0.195230335199157,0.0269726953471863,
0.0808855184856551));
#29727=CARTESIAN_POINT('Ctrl Pts',(-0.195118672945361,9.16100096969453E-5,
0.0824130307875757));
#29728=CARTESIAN_POINT('Origin',(0.,0.,0.));
#29729=CARTESIAN_POINT('',(-0.195279554503994,-0.000168121501241181,0.162586969212423));
#29730=CARTESIAN_POINT('',(-0.195287184048439,-0.0001702989282844,0.152413030787576));
#29731=CARTESIAN_POINT('',(-0.1954,-2.39295984553393E-17,0.));
#29732=CARTESIAN_POINT('Ctrl Pts',(-0.195279554503994,-0.000168121501241181,
0.162586969212423));
#29733=CARTESIAN_POINT('Ctrl Pts',(-0.194903656010943,0.0455834752155161,
0.159981723658113));
#29734=CARTESIAN_POINT('Ctrl Pts',(-0.178856730317397,0.091572573117829,
0.157376478103802));
#29735=CARTESIAN_POINT('Ctrl Pts',(-0.149500760249196,0.126316552728133,
0.154771232549492));
#29736=CARTESIAN_POINT('Ctrl Pts',(-0.107767134532898,0.175709989142681,
0.151067510866644));
#29737=CARTESIAN_POINT('Ctrl Pts',(-0.039135122029848,0.202376358702057,
0.147363789183796));
#29738=CARTESIAN_POINT('Ctrl Pts',(0.0249990333148566,0.194116955279127,
0.143660067500948));
#29739=CARTESIAN_POINT('Ctrl Pts',(0.0891331886595613,0.185857551856197,
0.139956345818101));
#29740=CARTESIAN_POINT('Ctrl Pts',(0.14876948684592,0.142672375450961,0.136252624135253));
#29741=CARTESIAN_POINT('Ctrl Pts',(0.176626827046517,0.0843167597229759,
0.132548902452405));
#29742=CARTESIAN_POINT('Ctrl Pts',(0.204484167247113,0.0259611439949913,
0.128845180769557));
#29743=CARTESIAN_POINT('Ctrl Pts',(0.200562549461947,-0.0475649110557425,
0.125141459086709));
#29744=CARTESIAN_POINT('Ctrl Pts',(0.166655969053473,-0.102626219289756,
0.121437737403861));
#29745=CARTESIAN_POINT('Ctrl Pts',(0.132749388644999,-0.157687527523771,
0.117734015721013));
#29746=CARTESIAN_POINT('Ctrl Pts',(0.0688578456132156,-0.194284088941065,
0.114030294038165));
#29747=CARTESIAN_POINT('Ctrl Pts',(0.00420898544956178,-0.19567474659654,
0.110326572355317));
#29748=CARTESIAN_POINT('Ctrl Pts',(-0.0604398747140919,-0.197065404252014,
0.106622850672469));
#29749=CARTESIAN_POINT('Ctrl Pts',(-0.125846052009616,-0.16325015814567,
0.102919128989622));
#29750=CARTESIAN_POINT('Ctrl Pts',(-0.162088905227235,-0.109697626925925,
0.0992154073067737));
#29751=CARTESIAN_POINT('Ctrl Pts',(-0.183709816073764,-0.0777505145902677,
0.0970059279419901));
#29752=CARTESIAN_POINT('Ctrl Pts',(-0.194952091996443,-0.0387793032173158,
0.0947964485772066));
#29753=CARTESIAN_POINT('Ctrl Pts',(-0.195128203910989,9.79727872364722E-5,
0.092586969212423));
#29754=CARTESIAN_POINT('Ctrl Pts',(-0.195118672945361,9.16100096969453E-5,
0.0824130307875757));
#29755=CARTESIAN_POINT('Ctrl Pts',(-0.194959408276249,-0.0382490737583375,
0.0845917324800272));
#29756=CARTESIAN_POINT('Ctrl Pts',(-0.184051065227066,-0.0766740948347571,
0.0867704341724787));
#29757=CARTESIAN_POINT('Ctrl Pts',(-0.162993550876047,-0.10835175828476,
0.0889491358649302));
#29758=CARTESIAN_POINT('Ctrl Pts',(-0.127172375978705,-0.162238988461419,
0.0926553498593023));
#29759=CARTESIAN_POINT('Ctrl Pts',(-0.0619817368257128,-0.196600853193387,
0.0963615638536743));
#29760=CARTESIAN_POINT('Ctrl Pts',(0.0027186436745272,-0.195701720127518,
0.100067777848046));
#29761=CARTESIAN_POINT('Ctrl Pts',(0.0674190241747668,-0.194802587061648,
0.103773991842418));
#29762=CARTESIAN_POINT('Ctrl Pts',(0.131629146022255,-0.15864245619794,
0.107480205836791));
#29763=CARTESIAN_POINT('Ctrl Pts',(0.165939903784035,-0.103781956343241,
0.111186419831163));
#29764=CARTESIAN_POINT('Ctrl Pts',(0.200250661545815,-0.0489214564885407,
0.114892633825535));
#29765=CARTESIAN_POINT('Ctrl Pts',(0.204662055221888,0.0246394123571516,
0.118598847819907));
#29766=CARTESIAN_POINT('Ctrl Pts',(0.177153295980734,0.0832073910176122,
0.122305061814279));
#29767=CARTESIAN_POINT('Ctrl Pts',(0.149644536739581,0.141775369678073,
0.126011275808651));
#29768=CARTESIAN_POINT('Ctrl Pts',(0.0902156245812001,0.185350458153303,
0.129717489803023));
#29769=CARTESIAN_POINT('Ctrl Pts',(0.0260864347694114,0.193974733338565,
0.133423703797395));
#29770=CARTESIAN_POINT('Ctrl Pts',(-0.0380427550423769,0.202599008523827,
0.137129917791767));
#29771=CARTESIAN_POINT('Ctrl Pts',(-0.106872222507573,0.176272470419122,
0.140836131786139));
#29772=CARTESIAN_POINT('Ctrl Pts',(-0.148876654315921,0.127053027794487,
0.144542345780511));
#29773=CARTESIAN_POINT('Ctrl Pts',(-0.178610829781436,0.0922114770268632,
0.147165907449533));
#29774=CARTESIAN_POINT('Ctrl Pts',(-0.194903067523895,0.0458983666015645,
0.149789469118554));
#29775=CARTESIAN_POINT('Ctrl Pts',(-0.195287184048439,-0.0001702989282844,
0.152413030787576));
#29776=CARTESIAN_POINT('Origin',(0.,0.,0.));
#29777=CARTESIAN_POINT('',(-0.19571996697324,4.08272333451705E-6,0.232586969212423));
#29778=CARTESIAN_POINT('',(-0.195720915199432,4.37834080700025E-6,0.222413030787575));
#29779=CARTESIAN_POINT('',(-0.1954,-2.39295984553393E-17,0.));
#29780=CARTESIAN_POINT('Ctrl Pts',(-0.19571996697324,4.08272333451705E-6,
0.232586969212423));
#29781=CARTESIAN_POINT('Ctrl Pts',(-0.19573993069631,0.0648866965015804,
0.228870720421867));
#29782=CARTESIAN_POINT('Ctrl Pts',(-0.160252793092098,0.129750264469882,
0.225154471631311));
#29783=CARTESIAN_POINT('Ctrl Pts',(-0.105631192010051,0.164767712566922,
0.221438222840754));
#29784=CARTESIAN_POINT('Ctrl Pts',(-0.0511937149515876,0.19966712030426,
0.217734501157906));
#29785=CARTESIAN_POINT('Ctrl Pts',(0.0222490761444335,0.204921286910345,
0.214030779475058));
#29786=CARTESIAN_POINT('Ctrl Pts',(0.0811002035332165,0.178126653559889,
0.210327057792211));
#29787=CARTESIAN_POINT('Ctrl Pts',(0.139951330921999,0.151332020209433,
0.206623336109363));
#29788=CARTESIAN_POINT('Ctrl Pts',(0.184210794603544,0.0924885869024359,
0.202919614426515));
#29789=CARTESIAN_POINT('Ctrl Pts',(0.193631757329266,0.028514740055385,
0.199215892743667));
#29790=CARTESIAN_POINT('Ctrl Pts',(0.203052720054988,-0.0354591067916664,
0.195512171060819));
#29791=CARTESIAN_POINT('Ctrl Pts',(0.177635181824887,-0.104563367178771,
0.191808449377971));
#29792=CARTESIAN_POINT('Ctrl Pts',(0.129006594271768,-0.147185755477259,
0.188104727695123));
#29793=CARTESIAN_POINT('Ctrl Pts',(0.0803780067186484,-0.189808143775746,
0.184401006012275));
#29794=CARTESIAN_POINT('Ctrl Pts',(0.00853836984250916,-0.205948659985616,
0.180697284329427));
#29795=CARTESIAN_POINT('Ctrl Pts',(-0.0536487147273854,-0.188223703762279,
0.176993562646579));
#29796=CARTESIAN_POINT('Ctrl Pts',(-0.11583579929728,-0.170498747538942,
0.173289840963732));
#29797=CARTESIAN_POINT('Ctrl Pts',(-0.168370331560931,-0.118908318882399,
0.169586119280884));
#29798=CARTESIAN_POINT('Ctrl Pts',(-0.187219978227984,-0.0570528529192665,
0.165882397598036));
#29799=CARTESIAN_POINT('Ctrl Pts',(-0.192810540551016,-0.0387073187246384,
0.164783921469498));
#29800=CARTESIAN_POINT('Ctrl Pts',(-0.195438048401311,-0.0194588316428207,
0.163685445340961));
#29801=CARTESIAN_POINT('Ctrl Pts',(-0.195279554503994,-0.000168121501241181,
0.162586969212423));
#29802=CARTESIAN_POINT('Ctrl Pts',(-0.195287184048439,-0.0001702989282844,
0.152413030787576));
#29803=CARTESIAN_POINT('Ctrl Pts',(-0.195445695530526,-0.0191812291650776,
0.153495683112926));
#29804=CARTESIAN_POINT('Ctrl Pts',(-0.192895173588402,-0.0381505322742495,
0.154578335438277));
#29805=CARTESIAN_POINT('Ctrl Pts',(-0.187462310228399,-0.0562548805321496,
0.155660987763628));
#29806=CARTESIAN_POINT('Ctrl Pts',(-0.168864138181028,-0.118230999089587,
0.159367201758));
#29807=CARTESIAN_POINT('Ctrl Pts',(-0.116488397934787,-0.170070889059896,
0.163073415752372));
#29808=CARTESIAN_POINT('Ctrl Pts',(-0.0543243355780667,-0.188030816136644,
0.166779629746744));
#29809=CARTESIAN_POINT('Ctrl Pts',(0.0078397267786532,-0.205990743213392,
0.170485843741116));
#29810=CARTESIAN_POINT('Ctrl Pts',(0.0797921112458524,-0.190070707396579,
0.174192057735488));
#29811=CARTESIAN_POINT('Ctrl Pts',(0.128577075941843,-0.147562399010748,
0.17789827172986));
#29812=CARTESIAN_POINT('Ctrl Pts',(0.177362040637834,-0.105054090624917,
0.181604485724232));
#29813=CARTESIAN_POINT('Ctrl Pts',(0.202979585562615,-0.0359575096700667,
0.185310699718604));
#29814=CARTESIAN_POINT('Ctrl Pts',(0.193696313672928,0.028079594435252,
0.189016913712976));
#29815=CARTESIAN_POINT('Ctrl Pts',(0.184413041783241,0.0921166985405712,
0.192723127707349));
#29816=CARTESIAN_POINT('Ctrl Pts',(0.140228953079084,0.151094325796358,
0.196429341701721));
#29817=CARTESIAN_POINT('Ctrl Pts',(0.0813813216582781,0.177999452248681,
0.200135555696093));
#29818=CARTESIAN_POINT('Ctrl Pts',(0.0225336902374724,0.204904578701004,
0.203841769690465));
#29819=CARTESIAN_POINT('Ctrl Pts',(-0.0509774838999832,0.199737204349863,
0.207547983684837));
#29820=CARTESIAN_POINT('Ctrl Pts',(-0.105482489992153,0.164864094185095,
0.211254197679209));
#29821=CARTESIAN_POINT('Ctrl Pts',(-0.16018451812442,0.129864926401004,
0.214973808715331));
#29822=CARTESIAN_POINT('Ctrl Pts',(-0.195742302622205,0.0649448754401196,
0.218693419751453));
#29823=CARTESIAN_POINT('Ctrl Pts',(-0.195720915199432,4.37834080700025E-6,
0.222413030787575));
#29824=CARTESIAN_POINT('Origin',(0.,0.,0.));
#29825=CARTESIAN_POINT('',(-0.195267691385146,0.000165493661177622,0.302586969212423));
#29826=CARTESIAN_POINT('',(-0.195274315056508,0.000167675988910205,0.292413030787576));
#29827=CARTESIAN_POINT('',(-0.1954,-2.39295984553393E-17,0.));
#29828=CARTESIAN_POINT('Ctrl Pts',(-0.195267691385146,0.000165493661177622,
0.302586969212423));
#29829=CARTESIAN_POINT('Ctrl Pts',(-0.195426560914452,0.0198992208020636,
0.301463438868469));
#29830=CARTESIAN_POINT('Ctrl Pts',(-0.192675342506316,0.0395896803504792,
0.300339908524515));
#29831=CARTESIAN_POINT('Ctrl Pts',(-0.186830808103941,0.0583146374609883,
0.29921637818056));
#29832=CARTESIAN_POINT('Ctrl Pts',(-0.167564280138135,0.120041523640586,
0.295512656497712));
#29833=CARTESIAN_POINT('Ctrl Pts',(-0.114682887836242,0.171276357431471,
0.291808934814864));
#29834=CARTESIAN_POINT('Ctrl Pts',(-0.0523776367443795,0.188581364320311,
0.288105213132016));
#29835=CARTESIAN_POINT('Ctrl Pts',(0.00992761434748341,0.20588637120915,
0.284401491449168));
#29836=CARTESIAN_POINT('Ctrl Pts',(0.0816567242293159,0.189261551195942,
0.280697769766321));
#29837=CARTESIAN_POINT('Ctrl Pts',(0.129996651882171,0.146312057934516,
0.276994048083473));
#29838=CARTESIAN_POINT('Ctrl Pts',(0.178336579535026,0.103362564673089,
0.273290326400625));
#29839=CARTESIAN_POINT('Ctrl Pts',(0.203287324958903,0.0340883981634439,
0.269586604717777));
#29840=CARTESIAN_POINT('Ctrl Pts',(0.193434974962867,-0.0298204336020968,
0.265882883034929));
#29841=CARTESIAN_POINT('Ctrl Pts',(0.183582624966831,-0.0937292653676373,
0.262179161352081));
#29842=CARTESIAN_POINT('Ctrl Pts',(0.138927179550881,-0.152272762389073,
0.258475439669233));
#29843=CARTESIAN_POINT('Ctrl Pts',(0.0798966206784796,-0.178669745083631,
0.254771717986385));
#29844=CARTESIAN_POINT('Ctrl Pts',(0.0208660618060775,-0.205066727778188,
0.251067996303538));
#29845=CARTESIAN_POINT('Ctrl Pts',(-0.0525396105227766,-0.199317196145866,
0.24736427462069));
#29846=CARTESIAN_POINT('Ctrl Pts',(-0.10674039873032,-0.16405131839538,
0.243660552937842));
#29847=CARTESIAN_POINT('Ctrl Pts',(-0.160757863467609,-0.128904720517098,
0.239969358362702));
#29848=CARTESIAN_POINT('Ctrl Pts',(-0.195700137841649,-0.0644411052866131,
0.236278163787563));
#29849=CARTESIAN_POINT('Ctrl Pts',(-0.19571996697324,4.08272333451705E-6,
0.232586969212423));
#29850=CARTESIAN_POINT('Ctrl Pts',(-0.195720915199432,4.37834080700025E-6,
0.222413030787575));
#29851=CARTESIAN_POINT('Ctrl Pts',(-0.195699681840184,-0.0644683222376,
0.226105847740198));
#29852=CARTESIAN_POINT('Ctrl Pts',(-0.160725113883781,-0.128960760246236,
0.22979866469282));
#29853=CARTESIAN_POINT('Ctrl Pts',(-0.106669244200308,-0.164098742623895,
0.233491481645442));
#29854=CARTESIAN_POINT('Ctrl Pts',(-0.0524172671136578,-0.199364200861572,
0.237197695639814));
#29855=CARTESIAN_POINT('Ctrl Pts',(0.0210547116140745,-0.205061829112049,
0.240903909634186));
#29856=CARTESIAN_POINT('Ctrl Pts',(0.0800949322066953,-0.178581989384044,
0.244610123628558));
#29857=CARTESIAN_POINT('Ctrl Pts',(0.139135152799316,-0.152102149656038,
0.24831633762293));
#29858=CARTESIAN_POINT('Ctrl Pts',(0.183743615256826,-0.0934448419495488,
0.252022551617302));
#29859=CARTESIAN_POINT('Ctrl Pts',(0.193488676008295,-0.0294763859316313,
0.255728765611674));
#29860=CARTESIAN_POINT('Ctrl Pts',(0.203233736759764,0.0344920700862864,
0.259434979606046));
#29861=CARTESIAN_POINT('Ctrl Pts',(0.178115395805193,0.103771674415633,
0.263141193600418));
#29862=CARTESIAN_POINT('Ctrl Pts',(0.129638398231036,0.146630865646616,
0.26684740759479));
#29863=CARTESIAN_POINT('Ctrl Pts',(0.0811614006568792,0.1894900568776,0.270553621589162));
#29864=CARTESIAN_POINT('Ctrl Pts',(0.00932574646313782,0.205928835010221,
0.274259835583535));
#29865=CARTESIAN_POINT('Ctrl Pts',(-0.0529662765081927,0.188417882975093,
0.277966049577907));
#29866=CARTESIAN_POINT('Ctrl Pts',(-0.115258299479523,0.170906930939964,
0.281672263572279));
#29867=CARTESIAN_POINT('Ctrl Pts',(-0.168006691228442,0.119446248737086,
0.285378477566651));
#29868=CARTESIAN_POINT('Ctrl Pts',(-0.187051544101399,0.0576059451476712,
0.289084691561023));
#29869=CARTESIAN_POINT('Ctrl Pts',(-0.192752575844056,0.0390941962730205,
0.290194137969874));
#29870=CARTESIAN_POINT('Ctrl Pts',(-0.195433466869055,0.0196523398123763,
0.291303584378725));
#29871=CARTESIAN_POINT('Ctrl Pts',(-0.195274315056508,0.000167675988910205,
0.292413030787576));
#29872=CARTESIAN_POINT('Origin',(0.,0.,0.));
#29873=CARTESIAN_POINT('',(-0.195135107115213,-0.000103745302926256,0.372586969212423));
#29874=CARTESIAN_POINT('',(-0.195125983814034,-9.67513988672578E-5,0.362413030787576));
#29875=CARTESIAN_POINT('',(-0.1954,-2.39295984553393E-17,0.));
#29876=CARTESIAN_POINT('Ctrl Pts',(-0.195135107115213,-0.000103745302926256,
0.372586969212423));
#29877=CARTESIAN_POINT('Ctrl Pts',(-0.19494564270682,0.0392108141373472,
0.370352435632223));
#29878=CARTESIAN_POINT('Ctrl Pts',(-0.183428685915158,0.078627490539017,
0.368117902052023));
#29879=CARTESIAN_POINT('Ctrl Pts',(-0.161345116677478,0.110788542383069,
0.365883368471823));
#29880=CARTESIAN_POINT('Ctrl Pts',(-0.124741775852795,0.164095230684139,
0.362179646788975));
#29881=CARTESIAN_POINT('Ctrl Pts',(-0.0591089924893776,0.197468687095231,
0.358475925106126));
#29882=CARTESIAN_POINT('Ctrl Pts',(0.00552900452708404,0.195641963566092,
0.354772203423278));
#29883=CARTESIAN_POINT('Ctrl Pts',(0.0701670015435453,0.193815240036952,
0.351068481740431));
#29884=CARTESIAN_POINT('Ctrl Pts',(0.13381021221305,0.156788336567581,0.347364760057583));
#29885=CARTESIAN_POINT('Ctrl Pts',(0.16734455320356,0.101499499073225,0.343661038374735));
#29886=CARTESIAN_POINT('Ctrl Pts',(0.20087889419407,0.0462106615788698,
0.339957316691887));
#29887=CARTESIAN_POINT('Ctrl Pts',(0.204304365505584,-0.0273401099404705,
0.336253595009039));
#29888=CARTESIAN_POINT('Ctrl Pts',(0.176053958557416,-0.0855064411333041,
0.332549873326191));
#29889=CARTESIAN_POINT('Ctrl Pts',(0.147803551609248,-0.143672772326139,
0.328846151643343));
#29890=CARTESIAN_POINT('Ctrl Pts',(0.0878772664013962,-0.186454663192466,
0.325142429960495));
#29891=CARTESIAN_POINT('Ctrl Pts',(0.0236888497103484,-0.194281203925035,
0.321438708277648));
#29892=CARTESIAN_POINT('Ctrl Pts',(-0.0404995669806982,-0.202107744657604,
0.3177349865948));
#29893=CARTESIAN_POINT('Ctrl Pts',(-0.108950115154941,-0.174978935256416,
0.314031264911952));
#29894=CARTESIAN_POINT('Ctrl Pts',(-0.150349557427203,-0.125305061271667,
0.310327543229104));
#29895=CARTESIAN_POINT('Ctrl Pts',(-0.179190407667273,-0.0906998424134863,
0.30774735189021));
#29896=CARTESIAN_POINT('Ctrl Pts',(-0.194902846959061,-0.0451530792879088,
0.305167160551317));
#29897=CARTESIAN_POINT('Ctrl Pts',(-0.195267691385146,0.000165493661177622,
0.302586969212423));
#29898=CARTESIAN_POINT('Ctrl Pts',(-0.195274315056508,0.000167675988910205,
0.292413030787576));
#29899=CARTESIAN_POINT('Ctrl Pts',(-0.194901804708373,-0.045438081105706,
0.295009798373097));
#29900=CARTESIAN_POINT('Ctrl Pts',(-0.178970412039892,-0.0912783539307832,
0.297606565958618));
#29901=CARTESIAN_POINT('Ctrl Pts',(-0.149789482266332,-0.125975537577289,
0.300203333544139));
#29902=CARTESIAN_POINT('Ctrl Pts',(-0.108141253561316,-0.175496791736879,
0.303909547538511));
#29903=CARTESIAN_POINT('Ctrl Pts',(-0.03950348215429,-0.202319375080107,
0.307615761532883));
#29904=CARTESIAN_POINT('Ctrl Pts',(0.0246862437687336,-0.194157962588032,
0.311321975527255));
#29905=CARTESIAN_POINT('Ctrl Pts',(0.0888759696917571,-0.185996550095957,
0.315028189521628));
#29906=CARTESIAN_POINT('Ctrl Pts',(0.148617650130778,-0.14285114176858,
0.318734403516));
#29907=CARTESIAN_POINT('Ctrl Pts',(0.176548299529208,-0.084483270534745,
0.322440617510372));
#29908=CARTESIAN_POINT('Ctrl Pts',(0.204478948927638,-0.0261153993009101,
0.326146831504744));
#29909=CARTESIAN_POINT('Ctrl Pts',(0.200598567285476,0.0474749348393822,
0.329853045499116));
#29910=CARTESIAN_POINT('Ctrl Pts',(0.166684453569178,0.102581762536563,
0.333559259493488));
#29911=CARTESIAN_POINT('Ctrl Pts',(0.13277033985288,0.157688590233743,0.33726547348786));
#29912=CARTESIAN_POINT('Ctrl Pts',(0.0688224940624468,0.194311911487812,
0.340971687482232));
#29913=CARTESIAN_POINT('Ctrl Pts',(0.00413041672205065,0.195677450731496,
0.344677901476604));
#29914=CARTESIAN_POINT('Ctrl Pts',(-0.0605616606183457,0.19704298997518,
0.348384115470976));
#29915=CARTESIAN_POINT('Ctrl Pts',(-0.125997969508704,0.163150747208479,
0.352090329465349));
#29916=CARTESIAN_POINT('Ctrl Pts',(-0.162207261036362,0.109524104808107,
0.355796543459721));
#29917=CARTESIAN_POINT('Ctrl Pts',(-0.183754705311226,0.0776119342016343,
0.358002039235672));
#29918=CARTESIAN_POINT('Ctrl Pts',(-0.194952253842872,0.0387114015523011,
0.360207535011624));
#29919=CARTESIAN_POINT('Ctrl Pts',(-0.195125983814034,-9.67513988672578E-5,
0.362413030787576));
#29920=CARTESIAN_POINT('Origin',(0.,0.,0.));
#29921=CARTESIAN_POINT('',(-0.195645574651684,-0.000107576288577632,0.442586969212423));
#29922=CARTESIAN_POINT('',(-0.195628130950281,-0.000119277919923279,0.432413030787576));
#29923=CARTESIAN_POINT('',(-0.1954,-2.39295984553393E-17,0.));
#29924=CARTESIAN_POINT('Ctrl Pts',(-0.195645574651684,-0.000107576288577632,
0.442586969212423));
#29925=CARTESIAN_POINT('Ctrl Pts',(-0.195258201164419,0.0583617837825317,
0.439241432395977));
#29926=CARTESIAN_POINT('Ctrl Pts',(-0.167312331125722,0.117152394520949,
0.435895895579531));
#29927=CARTESIAN_POINT('Ctrl Pts',(-0.121525966387556,0.153420296221226,
0.432550358763085));
#29928=CARTESIAN_POINT('Ctrl Pts',(-0.070837553387317,0.193571166257503,
0.428846637080237));
#29929=CARTESIAN_POINT('Ctrl Pts',(0.00171598407939347,0.206118438706562,
0.425142915397389));
#29930=CARTESIAN_POINT('Ctrl Pts',(0.0629444641593513,0.18532226587955,
0.421439193714541));
#29931=CARTESIAN_POINT('Ctrl Pts',(0.124172944239309,0.164526093052537,
0.417735472031693));
#29932=CARTESIAN_POINT('Ctrl Pts',(0.174076366932515,0.110386474949453,
0.414031750348845));
#29933=CARTESIAN_POINT('Ctrl Pts',(0.189826022128925,0.0476700023258525,
0.410328028665997));
#29934=CARTESIAN_POINT('Ctrl Pts',(0.205575677325334,-0.0150464702977478,
0.406624306983149));
#29935=CARTESIAN_POINT('Ctrl Pts',(0.187171565024948,-0.086339797441863,
0.402920585300301));
#29936=CARTESIAN_POINT('Ctrl Pts',(0.143032790007833,-0.133596290298842,
0.399216863617453));
#29937=CARTESIAN_POINT('Ctrl Pts',(0.0988940149907184,-0.180852783155821,
0.395513141934605));
#29938=CARTESIAN_POINT('Ctrl Pts',(0.0290205772568748,-0.204072441725662,
0.391809420251758));
#29939=CARTESIAN_POINT('Ctrl Pts',(-0.0346233738762281,-0.192633252011348,
0.38810569856891));
#29940=CARTESIAN_POINT('Ctrl Pts',(-0.0982673250093302,-0.181194062297035,
0.384401976886062));
#29941=CARTESIAN_POINT('Ctrl Pts',(-0.155681789541692,-0.135096024298568,
0.380698255203214));
#29942=CARTESIAN_POINT('Ctrl Pts',(-0.1806020726649,-0.0754270452038098,
0.376994533520366));
#29943=CARTESIAN_POINT('Ctrl Pts',(-0.190487422217158,-0.0517576224744695,
0.375525345417718));
#29944=CARTESIAN_POINT('Ctrl Pts',(-0.19525967846073,-0.0259527562563923,
0.374056157315071));
#29945=CARTESIAN_POINT('Ctrl Pts',(-0.195135107115213,-0.000103745302926256,
0.372586969212423));
#29946=CARTESIAN_POINT('Ctrl Pts',(-0.195125983814034,-9.67513988672578E-5,
0.362413030787576));
#29947=CARTESIAN_POINT('Ctrl Pts',(-0.195244197476311,-0.0265035587897937,
0.363913749005996));
#29948=CARTESIAN_POINT('Ctrl Pts',(-0.190258326051973,-0.0528675939020291,
0.365414467224416));
#29949=CARTESIAN_POINT('Ctrl Pts',(-0.1799560505048,-0.0769580726996389,
0.366915185442837));
#29950=CARTESIAN_POINT('Ctrl Pts',(-0.154513274280624,-0.136452565772967,
0.370621399437209));
#29951=CARTESIAN_POINT('Ctrl Pts',(-0.0966454476673152,-0.18208050988558,
0.374327613431581));
#29952=CARTESIAN_POINT('Ctrl Pts',(-0.0328572905191125,-0.192943316874967,
0.378033827425953));
#29953=CARTESIAN_POINT('Ctrl Pts',(0.0309308666290907,-0.203806123864353,
0.381740041420325));
#29954=CARTESIAN_POINT('Ctrl Pts',(0.100639354312189,-0.179903793730513,
0.385446255414697));
#29955=CARTESIAN_POINT('Ctrl Pts',(0.144340173058911,-0.132184112162819,
0.389152469409069));
#29956=CARTESIAN_POINT('Ctrl Pts',(0.188040991805633,-0.0844644305951239,
0.392858683403441));
#29957=CARTESIAN_POINT('Ctrl Pts',(0.205734141615979,-0.0129273975935752,
0.396564897397814));
#29958=CARTESIAN_POINT('Ctrl Pts',(0.189315776078089,0.0496614739501458,
0.400271111392186));
#29959=CARTESIAN_POINT('Ctrl Pts',(0.172897410540198,0.112250345493866,
0.403977325386558));
#29960=CARTESIAN_POINT('Ctrl Pts',(0.122367529654071,0.165891055579759,
0.40768353938093));
#29961=CARTESIAN_POINT('Ctrl Pts',(0.0608699149567017,0.186014995417357,
0.411389753375302));
#29962=CARTESIAN_POINT('Ctrl Pts',(-0.000627699740667481,0.206138935254955,
0.415095967369674));
#29963=CARTESIAN_POINT('Ctrl Pts',(-0.0730930482492791,0.19274610484426,
0.418802181364046));
#29964=CARTESIAN_POINT('Ctrl Pts',(-0.123335429038162,0.151970711029871,
0.422508395358418));
#29965=CARTESIAN_POINT('Ctrl Pts',(-0.168092015819396,0.115647443240051,
0.425809940501471));
#29966=CARTESIAN_POINT('Ctrl Pts',(-0.195213599025838,0.0575947822566119,
0.429111485644523));
#29967=CARTESIAN_POINT('Ctrl Pts',(-0.195628130950281,-0.000119277919923279,
0.432413030787576));
#29968=CARTESIAN_POINT('Origin',(0.,0.,0.));
#29969=CARTESIAN_POINT('',(-0.195458266482996,0.000173443779922018,0.512586969212423));
#29970=CARTESIAN_POINT('',(-0.195491180920002,0.000168629508682236,0.502413030787576));
#29971=CARTESIAN_POINT('',(-0.1954,-2.39295984553393E-17,0.));
#29972=CARTESIAN_POINT('Ctrl Pts',(-0.195458266482996,0.000173443779922018,
0.512586969212423));
#29973=CARTESIAN_POINT('Ctrl Pts',(-0.195579683437623,0.013363129532035,
0.511834150842579));
#29974=CARTESIAN_POINT('Ctrl Pts',(-0.194358523444966,0.0265304620125551,
0.511081332472735));
#29975=CARTESIAN_POINT('Ctrl Pts',(-0.191712292268468,0.0394048828472761,
0.510328514102891));
#29976=CARTESIAN_POINT('Ctrl Pts',(-0.178693343503641,0.10274455880328,
0.506624792420043));
#29977=CARTESIAN_POINT('Ctrl Pts',(-0.131181246839585,0.158994452273665,
0.502921070737195));
#29978=CARTESIAN_POINT('Ctrl Pts',(-0.0709107816346671,0.18242261056952,
0.499217349054347));
#29979=CARTESIAN_POINT('Ctrl Pts',(-0.0106403164297495,0.205850768865374,
0.495513627371499));
#29980=CARTESIAN_POINT('Ctrl Pts',(0.0623885173160298,0.196457191986698,
0.491809905688651));
#29981=CARTESIAN_POINT('Ctrl Pts',(0.114768109757825,0.158539044975217,
0.488106184005803));
#29982=CARTESIAN_POINT('Ctrl Pts',(0.167147702199619,0.120620897963737,
0.484402462322955));
#29983=CARTESIAN_POINT('Ctrl Pts',(0.19887805333743,0.0541781808194522,
0.480698740640107));
#29984=CARTESIAN_POINT('Ctrl Pts',(0.195443866449662,-0.0103943670439598,
0.476995018957259));
#29985=CARTESIAN_POINT('Ctrl Pts',(0.192009679561895,-0.0749669149073727,
0.473291297274411));
#29986=CARTESIAN_POINT('Ctrl Pts',(0.153410954648549,-0.137669293489913,
0.469587575591563));
#29987=CARTESIAN_POINT('Ctrl Pts',(0.0973049796091196,-0.169817810439032,
0.465883853908716));
#29988=CARTESIAN_POINT('Ctrl Pts',(0.0411990045696909,-0.20196632738815,
0.462180132225868));
#29989=CARTESIAN_POINT('Ctrl Pts',(-0.0324142205958206,-0.203560982703848,
0.45847641054302));
#29990=CARTESIAN_POINT('Ctrl Pts',(-0.0898597516275757,-0.17387228886878,
0.454772688860172));
#29991=CARTESIAN_POINT('Ctrl Pts',(-0.147305282659331,-0.144183595033712,
0.451068967177324));
#29992=CARTESIAN_POINT('Ctrl Pts',(-0.18858311955733,-0.0832115520478776,
0.447365245494476));
#29993=CARTESIAN_POINT('Ctrl Pts',(-0.194810393739446,-0.0188482967432128,
0.443661523811628));
#29994=CARTESIAN_POINT('Ctrl Pts',(-0.19541262996613,-0.0126237620787308,
0.443303338945226));
#29995=CARTESIAN_POINT('Ctrl Pts',(-0.195687048211354,-0.00636751036633503,
0.442945154078825));
#29996=CARTESIAN_POINT('Ctrl Pts',(-0.195645574651684,-0.000107576288577632,
0.442586969212423));
#29997=CARTESIAN_POINT('Ctrl Pts',(-0.195628130950281,-0.000119277919923279,
0.432413030787576));
#29998=CARTESIAN_POINT('Ctrl Pts',(-0.195678939935296,-0.00719326340995119,
0.432817699638895));
#29999=CARTESIAN_POINT('Ctrl Pts',(-0.195328521122814,-0.014262162001596,
0.433222368490215));
#30000=CARTESIAN_POINT('Ctrl Pts',(-0.194560169264522,-0.0212853377401693,
0.433627037341534));
#30001=CARTESIAN_POINT('Ctrl Pts',(-0.187523115632842,-0.0856080354777335,
0.437333251335906));
#30002=CARTESIAN_POINT('Ctrl Pts',(-0.145429595300328,-0.146095473734778,
0.441039465330279));
#30003=CARTESIAN_POINT('Ctrl Pts',(-0.0875593536694013,-0.175043093699665,
0.444745679324651));
#30004=CARTESIAN_POINT('Ctrl Pts',(-0.0296891120384743,-0.203990713664554,
0.448451893319023));
#30005=CARTESIAN_POINT('Ctrl Pts',(0.0439578508908652,-0.201398515337285,
0.452158107313395));
#30006=CARTESIAN_POINT('Ctrl Pts',(0.09964962855145,-0.168453781781564,
0.455864321307767));
#30007=CARTESIAN_POINT('Ctrl Pts',(0.155341406212034,-0.135509048225843,
0.459570535302139));
#30008=CARTESIAN_POINT('Ctrl Pts',(0.193077998603865,-0.072211779441669,
0.463276749296511));
#30009=CARTESIAN_POINT('Ctrl Pts',(0.195575227831571,-0.00755349757277263,
0.466982963290883));
#30010=CARTESIAN_POINT('Ctrl Pts',(0.198072457059277,0.0571047842961237,
0.470689177285256));
#30011=CARTESIAN_POINT('Ctrl Pts',(0.16533032312286,0.123124079249743,0.474395391279627));
#30012=CARTESIAN_POINT('Ctrl Pts',(0.112345433605614,0.160266118112717,
0.478101605273999));
#30013=CARTESIAN_POINT('Ctrl Pts',(0.059360544088369,0.197408156975691,
0.481807819268371));
#30014=CARTESIAN_POINT('Ctrl Pts',(-0.0138671010097046,0.20567293974802,
0.485514033262744));
#30015=CARTESIAN_POINT('Ctrl Pts',(-0.0737976517839776,0.181275016640803,
0.489220247257116));
#30016=CARTESIAN_POINT('Ctrl Pts',(-0.133728202558251,0.156877093533586,
0.492926461251488));
#30017=CARTESIAN_POINT('Ctrl Pts',(-0.180361659008724,0.0998164645468222,
0.49663267524586));
#30018=CARTESIAN_POINT('Ctrl Pts',(-0.192338886510923,0.0362281355122108,
0.500338889240232));
#30019=CARTESIAN_POINT('Ctrl Pts',(-0.194573194011967,0.0243659678682544,
0.501030269756014));
#30020=CARTESIAN_POINT('Ctrl Pts',(-0.195601481281436,0.0122766393772507,
0.501721650271795));
#30021=CARTESIAN_POINT('Ctrl Pts',(-0.195491180920002,0.000168629508682236,
0.502413030787576));
#30022=CARTESIAN_POINT('Origin',(0.,0.,0.));
#30023=CARTESIAN_POINT('',(-0.19507978584999,-3.45334863967226E-6,0.582586969212423));
#30024=CARTESIAN_POINT('',(-0.195080468396925,1.8981806121043E-5,0.572413030787576));
#30025=CARTESIAN_POINT('',(-0.1954,-2.39295984553393E-17,0.));
#30026=CARTESIAN_POINT('Ctrl Pts',(-0.195079815420139,-3.45302974047446E-6,
0.582586969212423));
#30027=CARTESIAN_POINT('Ctrl Pts',(-0.195074640707532,0.0328120037045956,
0.580723147606333));
#30028=CARTESIAN_POINT('Ctrl Pts',(-0.187237758907749,0.0656297824114404,
0.578859326000243));
#30029=CARTESIAN_POINT('Ctrl Pts',(-0.1715829951129,0.0941574404236039,
0.576995504394152));
#30030=CARTESIAN_POINT('Ctrl Pts',(-0.14047439120071,0.150846613462089,
0.573291782711304));
#30031=CARTESIAN_POINT('Ctrl Pts',(-0.0784943311216198,0.190594846094957,
0.569588061028457));
#30032=CARTESIAN_POINT('Ctrl Pts',(-0.0139960769924853,0.195218999146749,
0.565884339345609));
#30033=CARTESIAN_POINT('Ctrl Pts',(0.0505021771366483,0.199843152198542,
0.562180617662761));
#30034=CARTESIAN_POINT('Ctrl Pts',(0.117518625315826,0.169343225669258,
0.558476895979913));
#30035=CARTESIAN_POINT('Ctrl Pts',(0.156396070392606,0.117671648942254,
0.554773174297065));
#30036=CARTESIAN_POINT('Ctrl Pts',(0.195273515469386,0.0660000722152496,
0.551069452614217));
#30037=CARTESIAN_POINT('Ctrl Pts',(0.206011957443768,-0.00684315470947738,
0.547365730931369));
#30038=CARTESIAN_POINT('Ctrl Pts',(0.183699012241942,-0.0675353292756691,
0.543662009248521));
#30039=CARTESIAN_POINT('Ctrl Pts',(0.161386067040115,-0.128227503841861,
0.539958287565673));
#30040=CARTESIAN_POINT('Ctrl Pts',(0.106021734662079,-0.176768626049519,
0.536254565882826));
#30041=CARTESIAN_POINT('Ctrl Pts',(0.0429328609649713,-0.190953180775813,
0.532550844199978));
#30042=CARTESIAN_POINT('Ctrl Pts',(-0.0201560127321352,-0.205137735502108,
0.52884712251713));
#30043=CARTESIAN_POINT('Ctrl Pts',(-0.0909694277483132,-0.184965722747041,
0.525143400834282));
#30044=CARTESIAN_POINT('Ctrl Pts',(-0.137113234823603,-0.139664987148696,
0.521439679151434));
#30045=CARTESIAN_POINT('Ctrl Pts',(-0.173877852911313,-0.103572077852157,
0.51848877583843));
#30046=CARTESIAN_POINT('Ctrl Pts',(-0.194982335358017,-0.0515275892214865,
0.515537872525427));
#30047=CARTESIAN_POINT('Ctrl Pts',(-0.195458266482996,0.000173443779922018,
0.512586969212423));
#30048=CARTESIAN_POINT('Ctrl Pts',(-0.195491180920002,0.000168629508682236,
0.502413030787576));
#30049=CARTESIAN_POINT('Ctrl Pts',(-0.195010205227512,-0.0526295513449078,
0.505427864266167));
#30050=CARTESIAN_POINT('Ctrl Pts',(-0.172879182329996,-0.105782955367232,
0.508442697744757));
#30051=CARTESIAN_POINT('Ctrl Pts',(-0.134689356786549,-0.142005289462677,
0.511457531223348));
#30052=CARTESIAN_POINT('Ctrl Pts',(-0.0877416010060499,-0.186534356320495,
0.51516374521772));
#30053=CARTESIAN_POINT('Ctrl Pts',(-0.0165250908911267,-0.205476460953673,
0.518869959212092));
#30054=CARTESIAN_POINT('Ctrl Pts',(0.0463414671012952,-0.190155708549211,
0.522576173206464));
#30055=CARTESIAN_POINT('Ctrl Pts',(0.109208025093718,-0.174834956144749,
0.526282387200837));
#30056=CARTESIAN_POINT('Ctrl Pts',(0.163724630963639,-0.125251346702646,
0.529988601195209));
#30057=CARTESIAN_POINT('Ctrl Pts',(0.184921496651671,-0.0641152489120857,
0.533694815189581));
#30058=CARTESIAN_POINT('Ctrl Pts',(0.206118362339704,-0.00297915112152539,
0.537401029183953));
#30059=CARTESIAN_POINT('Ctrl Pts',(0.193995487845847,0.0697094350174917,
0.541107243178325));
#30060=CARTESIAN_POINT('Ctrl Pts',(0.154105412656959,0.120657560296821,
0.544813457172697));
#30061=CARTESIAN_POINT('Ctrl Pts',(0.114215337468071,0.171605685576151,
0.548519671167069));
#30062=CARTESIAN_POINT('Ctrl Pts',(0.0465580615841514,0.200813349995792,
0.552225885161441));
#30063=CARTESIAN_POINT('Ctrl Pts',(-0.0178779150223708,0.194902809680635,
0.555932099155813));
#30064=CARTESIAN_POINT('Ctrl Pts',(-0.0823138916288934,0.188992269365477,
0.559638313150186));
#30065=CARTESIAN_POINT('Ctrl Pts',(-0.143528568958019,0.14796352431552,
0.563344527144558));
#30066=CARTESIAN_POINT('Ctrl Pts',(-0.173484296927877,0.0906086297567353,
0.56705074113893));
#30067=CARTESIAN_POINT('Ctrl Pts',(-0.187931321146693,0.0629475576708828,
0.568838171021812));
#30068=CARTESIAN_POINT('Ctrl Pts',(-0.195107725773013,0.031489133949035,
0.570625600904694));
#30069=CARTESIAN_POINT('Ctrl Pts',(-0.195080468396925,1.8981806121043E-5,
0.572413030787576));
#30070=CARTESIAN_POINT('Origin',(0.,0.,0.));
#30071=CARTESIAN_POINT('',(-0.195470932084261,-0.000171584046685047,0.652586969212424));
#30072=CARTESIAN_POINT('',(-0.195421427783755,-0.000177812761388513,0.642413030787576));
#30073=CARTESIAN_POINT('',(-0.1954,-2.39295984553393E-17,0.));
#30074=CARTESIAN_POINT('Ctrl Pts',(-0.195470932084261,-0.000171584046685047,
0.652586969212424));
#30075=CARTESIAN_POINT('Ctrl Pts',(-0.194992946923152,0.0519398730151351,
0.649612144370087));
#30076=CARTESIAN_POINT('Ctrl Pts',(-0.173506994162404,0.104399306729571,
0.64663731952775));
#30077=CARTESIAN_POINT('Ctrl Pts',(-0.136210733975536,0.140545308526766,
0.643662494685414));
#30078=CARTESIAN_POINT('Ctrl Pts',(-0.0897760782010601,0.185547867567989,
0.639958773002566));
#30079=CARTESIAN_POINT('Ctrl Pts',(-0.0188341937200331,0.205263315093338,
0.636255051319719));
#30080=CARTESIAN_POINT('Ctrl Pts',(0.0441620008484366,0.190672665791667,
0.632551329636871));
#30081=CARTESIAN_POINT('Ctrl Pts',(0.107158195416906,0.176082016489995,
0.628847607954023));
#30082=CARTESIAN_POINT('Ctrl Pts',(0.162208700072817,0.127185270361303,
0.625143886271175));
#30083=CARTESIAN_POINT('Ctrl Pts',(0.184130231899333,0.0663506254660481,
0.621440164588327));
#30084=CARTESIAN_POINT('Ctrl Pts',(0.20605176372585,0.00551598057079281,
0.617736442905479));
#30085=CARTESIAN_POINT('Ctrl Pts',(0.194844322722972,-0.0672565630910262,
0.614032721222632));
#30086=CARTESIAN_POINT('Ctrl Pts',(0.155634840229719,-0.118676637573315,
0.610328999539784));
#30087=CARTESIAN_POINT('Ctrl Pts',(0.116425357736466,-0.170096712055603,
0.606625277856936));
#30088=CARTESIAN_POINT('Ctrl Pts',(0.0492138337528384,-0.200164317358361,
0.602921556174087));
#30089=CARTESIAN_POINT('Ctrl Pts',(-0.0152532956197894,-0.195124792816734,
0.59921783449124));
#30090=CARTESIAN_POINT('Ctrl Pts',(-0.0797204249924167,-0.190085268275106,
0.595514112808392));
#30091=CARTESIAN_POINT('Ctrl Pts',(-0.141443159754043,-0.149938613889095,
0.591810391125544));
#30092=CARTESIAN_POINT('Ctrl Pts',(-0.172185953262212,-0.0930502299740384,
0.588106669442696));
#30093=CARTESIAN_POINT('Ctrl Pts',(-0.187458069522289,-0.0647897528391999,
0.586266769365939));
#30094=CARTESIAN_POINT('Ctrl Pts',(-0.195084923717034,-0.0323977343102287,
0.584426869289181));
#30095=CARTESIAN_POINT('Ctrl Pts',(-0.195079815420139,-3.45302974047446E-6,
0.582586969212423));
#30096=CARTESIAN_POINT('Ctrl Pts',(-0.195080468396925,1.8981806121043E-5,
0.572413030787576));
#30097=CARTESIAN_POINT('Ctrl Pts',(-0.195051207937167,-0.0337638415069996,
0.574331814899066));
#30098=CARTESIAN_POINT('Ctrl Pts',(-0.186720620393942,-0.0675601803708791,
0.576250599010555));
#30099=CARTESIAN_POINT('Ctrl Pts',(-0.170171536425399,-0.0966869859783203,
0.578169383122045));
#30100=CARTESIAN_POINT('Ctrl Pts',(-0.138206269342473,-0.15294666308698,
0.581875597116418));
#30101=CARTESIAN_POINT('Ctrl Pts',(-0.0755789565660301,-0.191784973236686,
0.585581811110791));
#30102=CARTESIAN_POINT('Ctrl Pts',(-0.0109742658556152,-0.195413127900566,
0.589288025105163));
#30103=CARTESIAN_POINT('Ctrl Pts',(0.0536304248547996,-0.199041282564447,
0.592994239099535));
#30104=CARTESIAN_POINT('Ctrl Pts',(0.120212493499187,-0.1674592817425,0.596700453093906));
#30105=CARTESIAN_POINT('Ctrl Pts',(0.158275908344154,-0.115132366886058,
0.600406667088278));
#30106=CARTESIAN_POINT('Ctrl Pts',(0.19633932318912,-0.0628054520296152,
0.60411288108265));
#30107=CARTESIAN_POINT('Ctrl Pts',(0.205884084234667,0.0102663768613233,
0.607819095077022));
#30108=CARTESIAN_POINT('Ctrl Pts',(0.182538483877546,0.0706146370849535,
0.611525309071394));
#30109=CARTESIAN_POINT('Ctrl Pts',(0.159192883520425,0.130962897308584,
0.615231523065767));
#30110=CARTESIAN_POINT('Ctrl Pts',(0.102956921760636,0.178587588864905,
0.618937737060139));
#30111=CARTESIAN_POINT('Ctrl Pts',(0.0395878889512919,0.191675569949154,
0.622643951054511));
#30112=CARTESIAN_POINT('Ctrl Pts',(-0.0237811438580523,0.204763551033402,
0.626350165048883));
#30113=CARTESIAN_POINT('Ctrl Pts',(-0.0942832477169518,0.183314821645578,
0.630056379043255));
#30114=CARTESIAN_POINT('Ctrl Pts',(-0.139626929730598,0.137153365109863,
0.633762593037627));
#30115=CARTESIAN_POINT('Ctrl Pts',(-0.17490486198241,0.101239194403086,
0.63664607228761));
#30116=CARTESIAN_POINT('Ctrl Pts',(-0.194954331224527,0.0503663409317413,
0.639529551537593));
#30117=CARTESIAN_POINT('Ctrl Pts',(-0.195421427783755,-0.000177812761388513,
0.642413030787576));
#30118=CARTESIAN_POINT('Origin',(0.,0.,0.));
#30119=CARTESIAN_POINT('',(-0.195636369417486,0.000113518110994186,0.722586969212423));
#30120=CARTESIAN_POINT('',(-0.195675615924934,8.51174274233985E-5,0.712413030787576));
#30121=CARTESIAN_POINT('',(-0.1954,-2.39295984553393E-17,0.));
#30122=CARTESIAN_POINT('Ctrl Pts',(-0.195636369417486,0.000113518110994186,
0.722586969212423));
#30123=CARTESIAN_POINT('Ctrl Pts',(-0.195682546989371,0.00679235189129894,
0.722204862816689));
#30124=CARTESIAN_POINT('Ctrl Pts',(-0.195370156992351,0.0134668159558925,
0.721822756420955));
#30125=CARTESIAN_POINT('Ctrl Pts',(-0.194684940168549,0.0201027826582277,
0.72144065002522));
#30126=CARTESIAN_POINT('Ctrl Pts',(-0.188043197355288,0.0844245894546327,
0.717736928342373));
#30127=CARTESIAN_POINT('Ctrl Pts',(-0.146373463610807,0.145129475044757,
0.714033206659525));
#30128=CARTESIAN_POINT('Ctrl Pts',(-0.0887378837876281,0.174447515831938,
0.710329484976677));
#30129=CARTESIAN_POINT('Ctrl Pts',(-0.031102303964449,0.203765556619118,
0.706625763293829));
#30130=CARTESIAN_POINT('Ctrl Pts',(0.0424991219374283,0.201696752603353,
0.702922041610981));
#30131=CARTESIAN_POINT('Ctrl Pts',(0.0983968473233738,0.169187494324663,
0.699218319928133));
#30132=CARTESIAN_POINT('Ctrl Pts',(0.154294572709319,0.136678236045973,
0.695514598245285));
#30133=CARTESIAN_POINT('Ctrl Pts',(0.192488597579333,0.0737285235043576,
0.691810876562437));
#30134=CARTESIAN_POINT('Ctrl Pts',(0.195506767226643,0.00913519390189264,
0.68810715487959));
#30135=CARTESIAN_POINT('Ctrl Pts',(0.198524936873952,-0.0554581357005719,
0.684403433196742));
#30136=CARTESIAN_POINT('Ctrl Pts',(0.166367251298559,-0.121695082363886,
0.680699711513894));
#30137=CARTESIAN_POINT('Ctrl Pts',(0.113744494695038,-0.159275037986524,
0.676995989831046));
#30138=CARTESIAN_POINT('Ctrl Pts',(0.0611217380915185,-0.196854993609162,
0.673292268148198));
#30139=CARTESIAN_POINT('Ctrl Pts',(-0.0119660895401274,-0.205777958191125,
0.669588546465349));
#30140=CARTESIAN_POINT('Ctrl Pts',(-0.072084391141631,-0.181962051958034,
0.665884824782502));
#30141=CARTESIAN_POINT('Ctrl Pts',(-0.132202692743136,-0.158146145724943,
0.662181103099654));
#30142=CARTESIAN_POINT('Ctrl Pts',(-0.179351468314497,-0.101591368676797,
0.658477381416807));
#30143=CARTESIAN_POINT('Ctrl Pts',(-0.191962142566216,-0.0381691448741754,
0.654773659733959));
#30144=CARTESIAN_POINT('Ctrl Pts',(-0.19444393828574,-0.0256875756563692,
0.654044762893447));
#30145=CARTESIAN_POINT('Ctrl Pts',(-0.195588048853217,-0.0129400253566584,
0.653315866052935));
#30146=CARTESIAN_POINT('Ctrl Pts',(-0.195470932084261,-0.000171584046685047,
0.652586969212424));
#30147=CARTESIAN_POINT('Ctrl Pts',(-0.195421427783755,-0.000177812761388513,
0.642413030787576));
#30148=CARTESIAN_POINT('Ctrl Pts',(-0.195554703085897,-0.0145994290672205,
0.643235765531965));
#30149=CARTESIAN_POINT('Ctrl Pts',(-0.194093747105224,-0.0289942854151266,
0.644058500276354));
#30150=CARTESIAN_POINT('Ctrl Pts',(-0.190937423221194,-0.0430072724152966,
0.644881235020743));
#30151=CARTESIAN_POINT('Ctrl Pts',(-0.17671897452975,-0.106132269721135,
0.648587449015115));
#30152=CARTESIAN_POINT('Ctrl Pts',(-0.128096816978468,-0.161508080649208,
0.652293663009487));
#30153=CARTESIAN_POINT('Ctrl Pts',(-0.067340953434779,-0.183771382585667,
0.65599987700386));
#30154=CARTESIAN_POINT('Ctrl Pts',(-0.00658508989108841,-0.206034684522128,
0.659706090998232));
#30155=CARTESIAN_POINT('Ctrl Pts',(0.06630447964501,-0.195185477466974,
0.663412304992604));
#30156=CARTESIAN_POINT('Ctrl Pts',(0.117942751209788,-0.156192933591821,
0.667118518986976));
#30157=CARTESIAN_POINT('Ctrl Pts',(0.169581022774564,-0.117200389716668,
0.670824732981348));
#30158=CARTESIAN_POINT('Ctrl Pts',(0.19996799636802,-0.0500645090215166,
0.67453094697572));
#30159=CARTESIAN_POINT('Ctrl Pts',(0.195185778931935,0.0144650188277344,
0.678237160970092));
#30160=CARTESIAN_POINT('Ctrl Pts',(0.190403561495849,0.0789945466769872,
0.681943374964464));
#30161=CARTESIAN_POINT('Ctrl Pts',(0.15045215303022,0.14091772168034,0.685649588958836));
#30162=CARTESIAN_POINT('Ctrl Pts',(0.0936301652358751,0.171872386452436,
0.689355802953208));
#30163=CARTESIAN_POINT('Ctrl Pts',(0.0368081774415317,0.202827051224532,
0.69306201694758));
#30164=CARTESIAN_POINT('Ctrl Pts',(-0.0368843896815252,0.202813205765373,
0.696768230941953));
#30165=CARTESIAN_POINT('Ctrl Pts',(-0.0936947418561655,0.171837191595589,
0.700474444936325));
#30166=CARTESIAN_POINT('Ctrl Pts',(-0.150505094030807,0.140861177425805,
0.704180658930697));
#30167=CARTESIAN_POINT('Ctrl Pts',(-0.190433231257031,0.078922994545395,
0.707886872925069));
#30168=CARTESIAN_POINT('Ctrl Pts',(-0.195191200566454,0.0143916742729559,
0.711593086919441));
#30169=CARTESIAN_POINT('Ctrl Pts',(-0.195542076848464,0.00963281429343837,
0.711866401542153));
#30170=CARTESIAN_POINT('Ctrl Pts',(-0.195701686505733,0.00485985200318871,
0.712139716164864));
#30171=CARTESIAN_POINT('Ctrl Pts',(-0.195675615924934,8.51174274233985E-5,
0.712413030787576));
#30172=CARTESIAN_POINT('Origin',(0.,0.,0.));
#30173=CARTESIAN_POINT('',(-0.195128545551857,9.80157954364874E-5,0.792586969212424));
#30174=CARTESIAN_POINT('',(-0.195166123101285,0.000126544742759004,0.782413030787576));
#30175=CARTESIAN_POINT('',(-0.1954,-2.39295984553393E-17,0.));
#30176=CARTESIAN_POINT('Ctrl Pts',(-0.195128545551857,9.80157954364874E-5,
0.792586969212424));
#30177=CARTESIAN_POINT('Ctrl Pts',(-0.195247914943593,0.0263701155015296,
0.791093859580443));
#30178=CARTESIAN_POINT('Ctrl Pts',(-0.190313505751618,0.0525992349613935,
0.789600749948463));
#30179=CARTESIAN_POINT('Ctrl Pts',(-0.180112460177197,0.0765888339627252,
0.788107640316483));
#30180=CARTESIAN_POINT('Ctrl Pts',(-0.154808334564134,0.136096050365993,
0.784403918633635));
#30181=CARTESIAN_POINT('Ctrl Pts',(-0.0970981193167941,0.181823294990903,
0.780700196950786));
#30182=CARTESIAN_POINT('Ctrl Pts',(-0.0333818027149729,0.192852282969788,
0.776996475267938));
#30183=CARTESIAN_POINT('Ctrl Pts',(0.0303345138868501,0.203881270948674,
0.773292753585091));
#30184=CARTESIAN_POINT('Ctrl Pts',(0.100056931843154,0.180212002281536,
0.769589031902244));
#30185=CARTESIAN_POINT('Ctrl Pts',(0.143890387011628,0.132672168613705,
0.765885310219396));
#30186=CARTESIAN_POINT('Ctrl Pts',(0.187723842180101,0.0851323349458752,
0.762181588536548));
#30187=CARTESIAN_POINT('Ctrl Pts',(0.205668334560742,0.013721936277351,
0.758477866853699));
#30188=CARTESIAN_POINT('Ctrl Pts',(0.18951501609247,-0.0488917833023672,
0.754774145170851));
#30189=CARTESIAN_POINT('Ctrl Pts',(0.173361697624198,-0.111505502882086,
0.751070423488003));
#30190=CARTESIAN_POINT('Ctrl Pts',(0.123110568307013,-0.165322543373001,
0.747366701805156));
#30191=CARTESIAN_POINT('Ctrl Pts',(0.061749399359133,-0.185723879665063,
0.743662980122308));
#30192=CARTESIAN_POINT('Ctrl Pts',(0.000388230411252383,-0.206125215957126,
0.73995925843946));
#30193=CARTESIAN_POINT('Ctrl Pts',(-0.072082978167322,-0.193110848050335,
0.736255536756612));
#30194=CARTESIAN_POINT('Ctrl Pts',(-0.122511706515588,-0.152634300095596,
0.732551815073764));
#30195=CARTESIAN_POINT('Ctrl Pts',(-0.16773779241913,-0.116333645789233,
0.72923019978665));
#30196=CARTESIAN_POINT('Ctrl Pts',(-0.195234952088687,-0.0579449614967985,
0.725908584499537));
#30197=CARTESIAN_POINT('Ctrl Pts',(-0.195636369417486,0.000113518110994186,
0.722586969212423));
#30198=CARTESIAN_POINT('Ctrl Pts',(-0.195675615924934,8.51174274233985E-5,
0.712413030787576));
#30199=CARTESIAN_POINT('Ctrl Pts',(-0.195348162971424,-0.0598867317271105,
0.715845930159236));
#30200=CARTESIAN_POINT('Ctrl Pts',(-0.165727828481393,-0.120138176331325,
0.719278829530897));
#30201=CARTESIAN_POINT('Ctrl Pts',(-0.117884051406102,-0.156237241050387,
0.722711728902558));
#30202=CARTESIAN_POINT('Ctrl Pts',(-0.0662311315437018,-0.195210378436822,
0.72641794289693));
#30203=CARTESIAN_POINT('Ctrl Pts',(0.00666250957372189,-0.206032195545224,
0.730124156891302));
#30204=CARTESIAN_POINT('Ctrl Pts',(0.0674100031098693,-0.183746065393738,
0.733830370885674));
#30205=CARTESIAN_POINT('Ctrl Pts',(0.128157496646017,-0.161459935242253,
0.737536584880046));
#30206=CARTESIAN_POINT('Ctrl Pts',(0.176758842600887,-0.10606585783088,
0.741242798874417));
#30207=CARTESIAN_POINT('Ctrl Pts',(0.19095357026966,-0.0429355222190436,
0.744949012868789));
#30208=CARTESIAN_POINT('Ctrl Pts',(0.205148297938434,0.0201948133927931,
0.748655226863161));
#30209=CARTESIAN_POINT('Ctrl Pts',(0.184936407321109,0.0910614072050953,
0.752361440857534));
#30210=CARTESIAN_POINT('Ctrl Pts',(0.139575382755531,0.137205822017881,
0.756067654851907));
#30211=CARTESIAN_POINT('Ctrl Pts',(0.0942143581899539,0.183350236830666,
0.759773868846279));
#30212=CARTESIAN_POINT('Ctrl Pts',(0.0237041996761252,0.204772472643938,
0.76348008284065));
#30213=CARTESIAN_POINT('Ctrl Pts',(-0.0396599106844383,0.191660680765389,
0.767186296835022));
#30214=CARTESIAN_POINT('Ctrl Pts',(-0.103024021045003,0.178548888886839,
0.770892510829394));
#30215=CARTESIAN_POINT('Ctrl Pts',(-0.159242083252301,0.130903069316467,
0.774598724823766));
#30216=CARTESIAN_POINT('Ctrl Pts',(-0.182565005336597,0.0705460409477194,
0.778304938818139));
#30217=CARTESIAN_POINT('Ctrl Pts',(-0.19118230851659,0.0482454556858425,
0.779674302807951));
#30218=CARTESIAN_POINT('Ctrl Pts',(-0.195308968355645,0.0242096139413284,
0.781043666797764));
#30219=CARTESIAN_POINT('Ctrl Pts',(-0.195166123101285,0.000126544742759004,
0.782413030787576));
#30220=CARTESIAN_POINT('Origin',(0.,0.,0.));
#30221=CARTESIAN_POINT('',(-0.195279013340439,-0.000168009551267251,0.862586969212423));
#30222=CARTESIAN_POINT('',(-0.195215444869335,-0.000150235120299324,0.852413030787576));
#30223=CARTESIAN_POINT('',(-0.1954,-2.39295984553393E-17,0.));
#30224=CARTESIAN_POINT('Ctrl Pts',(-0.195279013340439,-0.000168009551267251,
0.862586969212423));
#30225=CARTESIAN_POINT('Ctrl Pts',(-0.194903607268958,0.0455640131522026,
0.859982856344197));
#30226=CARTESIAN_POINT('Ctrl Pts',(-0.178871895344458,0.0915331173731693,
0.857378743475971));
#30227=CARTESIAN_POINT('Ctrl Pts',(-0.149539281844263,0.126270942713959,
0.854774630607745));
#30228=CARTESIAN_POINT('Ctrl Pts',(-0.107820722729247,0.175677110357261,
0.851070908924897));
#30229=CARTESIAN_POINT('Ctrl Pts',(-0.0391968436807465,0.202364430724413,
0.847367187242049));
#30230=CARTESIAN_POINT('Ctrl Pts',(0.024939826400162,0.194124580780539,
0.843663465559201));
#30231=CARTESIAN_POINT('Ctrl Pts',(0.0890764964810705,0.185884730836666,
0.839959743876352));
#30232=CARTESIAN_POINT('Ctrl Pts',(0.148725957594388,0.142717710581768,
0.836256022193505));
#30233=CARTESIAN_POINT('Ctrl Pts',(0.176601098282085,0.0843706103134459,
0.832552300510657));
#30234=CARTESIAN_POINT('Ctrl Pts',(0.204476238969783,0.0260235100451228,
0.828848578827809));
#30235=CARTESIAN_POINT('Ctrl Pts',(0.200577059231861,-0.0475036702366233,
0.825144857144961));
#30236=CARTESIAN_POINT('Ctrl Pts',(0.166687269277466,-0.102575348200379,
0.821441135462114));
#30237=CARTESIAN_POINT('Ctrl Pts',(0.132797479323072,-0.157647026164133,
0.817737413779266));
#30238=CARTESIAN_POINT('Ctrl Pts',(0.0689170791522051,-0.194263201809897,
0.814033692096418));
#30239=CARTESIAN_POINT('Ctrl Pts',(0.00426865627857745,-0.195673519857469,
0.81032997041357));
#30240=CARTESIAN_POINT('Ctrl Pts',(-0.060379766595052,-0.197083837905041,
0.806626248730722));
#30241=CARTESIAN_POINT('Ctrl Pts',(-0.125796212171444,-0.16328829835442,
0.802922527047874));
#30242=CARTESIAN_POINT('Ctrl Pts',(-0.162055416970245,-0.109746934488294,
0.799218805365026));
#30243=CARTESIAN_POINT('Ctrl Pts',(-0.183697171385623,-0.0777901098892797,
0.797008193314158));
#30244=CARTESIAN_POINT('Ctrl Pts',(-0.194951814111497,-0.0387989405753114,
0.794797581263291));
#30245=CARTESIAN_POINT('Ctrl Pts',(-0.195128545551857,9.80157954364874E-5,
0.792586969212424));
#30246=CARTESIAN_POINT('Ctrl Pts',(-0.195166123101285,0.000126544742759004,
0.782413030787576));
#30247=CARTESIAN_POINT('Ctrl Pts',(-0.194922354508138,-0.0409717467160323,
0.784749880792136));
#30248=CARTESIAN_POINT('Ctrl Pts',(-0.182244856716882,-0.0822075748123473,
0.787086730796695));
#30249=CARTESIAN_POINT('Ctrl Pts',(-0.158232634722073,-0.115191832939155,
0.789423580801255));
#30250=CARTESIAN_POINT('Ctrl Pts',(-0.120149560061961,-0.167504441290151,
0.793129794795627));
#30251=CARTESIAN_POINT('Ctrl Pts',(-0.0535556287804454,-0.199061420825021,
0.796836008789999));
#30252=CARTESIAN_POINT('Ctrl Pts',(0.0110476940437387,-0.195408990384897,
0.800542222784371));
#30253=CARTESIAN_POINT('Ctrl Pts',(0.0756510168679237,-0.191756559944773,
0.804248436778743));
#30254=CARTESIAN_POINT('Ctrl Pts',(0.138263731234777,-0.152894719529654,
0.807954650773115));
#30255=CARTESIAN_POINT('Ctrl Pts',(0.170207855773424,-0.0966230350379699,
0.811660864767488));
#30256=CARTESIAN_POINT('Ctrl Pts',(0.202151980312072,-0.0403513505462853,
0.81536707876186));
#30257=CARTESIAN_POINT('Ctrl Pts',(0.203427515022513,0.0333301780219651,
0.819073292756232));
#30258=CARTESIAN_POINT('Ctrl Pts',(0.173450237337761,0.0906738122863988,
0.822779506750604));
#30259=CARTESIAN_POINT('Ctrl Pts',(0.143472959653009,0.148017446550833,
0.826485720744976));
#30260=CARTESIAN_POINT('Ctrl Pts',(0.0822428695730641,0.189023186511451,
0.830191934739348));
#30261=CARTESIAN_POINT('Ctrl Pts',(0.0178046765554912,0.194909513773745,
0.83389814873372));
#30262=CARTESIAN_POINT('Ctrl Pts',(-0.0466335164620799,0.200795841036038,
0.837604362728092));
#30263=CARTESIAN_POINT('Ctrl Pts',(-0.114279812417278,0.171562755600011,
0.841310576722464));
#30264=CARTESIAN_POINT('Ctrl Pts',(-0.154150740386038,0.120599644714809,
0.845016790716836));
#30265=CARTESIAN_POINT('Ctrl Pts',(-0.180673309918174,0.0866984359672774,
0.84748220407375));
#30266=CARTESIAN_POINT('Ctrl Pts',(-0.194905131081074,0.0431815751432988,
0.849947617430663));
#30267=CARTESIAN_POINT('Ctrl Pts',(-0.195215444869335,-0.000150235120299324,
0.852413030787576));
#30268=CARTESIAN_POINT('Origin',(0.,0.,0.));
#30269=CARTESIAN_POINT('',(-0.195719986784682,3.71606954582295E-6,0.932586969212424));
#30270=CARTESIAN_POINT('',(-0.195707453392556,-4.66568259871601E-5,0.922413030787576));
#30271=CARTESIAN_POINT('',(-0.1954,-2.39295984553393E-17,0.));
#30272=CARTESIAN_POINT('Ctrl Pts',(-0.195719986784682,3.71606954582295E-6,
0.932586969212424));
#30273=CARTESIAN_POINT('Ctrl Pts',(-0.195738156138108,0.0648665395087412,
0.928871853107952));
#30274=CARTESIAN_POINT('Ctrl Pts',(-0.160275715576186,0.129712057687137,
0.925156737003479));
#30275=CARTESIAN_POINT('Ctrl Pts',(-0.10568144211536,0.164735485073218,
0.921441620899007));
#30276=CARTESIAN_POINT('Ctrl Pts',(-0.0512546116502832,0.199651494094127,
0.917737899216159));
#30277=CARTESIAN_POINT('Ctrl Pts',(0.0221865722997436,0.204928064005996,
0.914034177533311));
#30278=CARTESIAN_POINT('Ctrl Pts',(0.0810458692323854,0.178151382429043,
0.910330455850463));
#30279=CARTESIAN_POINT('Ctrl Pts',(0.139905166165026,0.151374700852089,
0.906626734167615));
#30280=CARTESIAN_POINT('Ctrl Pts',(0.184182576080283,0.0925447677863139,
0.902923012484767));
#30281=CARTESIAN_POINT('Ctrl Pts',(0.193623051178265,0.0285737974246437,
0.899219290801919));
#30282=CARTESIAN_POINT('Ctrl Pts',(0.203063526276248,-0.0353971729370283,
0.895515569119071));
#30283=CARTESIAN_POINT('Ctrl Pts',(0.177667066556955,-0.104509180594595,
0.891811847436224));
#30284=CARTESIAN_POINT('Ctrl Pts',(0.129051481285208,-0.147146399547075,
0.888108125753376));
#30285=CARTESIAN_POINT('Ctrl Pts',(0.0804358960134615,-0.189783618499555,
0.884404404070528));
#30286=CARTESIAN_POINT('Ctrl Pts',(0.00860118518926115,-0.205946048746948,
0.88070068238768));
#30287=CARTESIAN_POINT('Ctrl Pts',(-0.0535913025040727,-0.188240059832962,
0.876996960704832));
#30288=CARTESIAN_POINT('Ctrl Pts',(-0.115783790197406,-0.170534070918976,
0.873293239021984));
#30289=CARTESIAN_POINT('Ctrl Pts',(-0.168334054759872,-0.118959662843613,
0.869589517339136));
#30290=CARTESIAN_POINT('Ctrl Pts',(-0.187202567450341,-0.0571099513462054,
0.865885795656288));
#30291=CARTESIAN_POINT('Ctrl Pts',(-0.192804495632289,-0.0387472087407564,
0.864786186841667));
#30292=CARTESIAN_POINT('Ctrl Pts',(-0.195437531748109,-0.0194787452297348,
0.863686578027045));
#30293=CARTESIAN_POINT('Ctrl Pts',(-0.195279013340439,-0.000168009551267251,
0.862586969212423));
#30294=CARTESIAN_POINT('Ctrl Pts',(-0.195215444869335,-0.000150235120299324,
0.852413030787576));
#30295=CARTESIAN_POINT('Ctrl Pts',(-0.195371620524508,-0.021958398707372,
0.853653831425035));
#30296=CARTESIAN_POINT('Ctrl Pts',(-0.192001564940553,-0.0437196901383431,
0.854894632062494));
#30297=CARTESIAN_POINT('Ctrl Pts',(-0.184897391479539,-0.0641847309864828,
0.856135432699953));
#30298=CARTESIAN_POINT('Ctrl Pts',(-0.163677554621959,-0.125312859468192,
0.859841646694325));
#30299=CARTESIAN_POINT('Ctrl Pts',(-0.10914232092448,-0.174875980097234,
0.863547860688697));
#30300=CARTESIAN_POINT('Ctrl Pts',(-0.0462700104058479,-0.190173108515756,
0.867254074683069));
#30301=CARTESIAN_POINT('Ctrl Pts',(0.0166023001127845,-0.205470236934278,
0.870960288677441));
#30302=CARTESIAN_POINT('Ctrl Pts',(0.0878116874525705,-0.186501373142281,
0.874666502671813));
#30303=CARTESIAN_POINT('Ctrl Pts',(0.134742707561642,-0.141954668207959,
0.878372716666185));
#30304=CARTESIAN_POINT('Ctrl Pts',(0.181673727670714,-0.0974079632736377,
0.882078930660557));
#30305=CARTESIAN_POINT('Ctrl Pts',(0.204326380549072,-0.0272834171969915,
0.885785144654929));
#30306=CARTESIAN_POINT('Ctrl Pts',(0.192325259761237,0.0363004067433246,
0.889491358649301));
#30307=CARTESIAN_POINT('Ctrl Pts',(0.180324138973402,0.0998842306836407,
0.893197572643673));
#30308=CARTESIAN_POINT('Ctrl Pts',(0.133669244519374,0.156927332487627,
0.896903786638045));
#30309=CARTESIAN_POINT('Ctrl Pts',(0.0737295301650971,0.181302734225987,
0.900610000632418));
#30310=CARTESIAN_POINT('Ctrl Pts',(0.0137898158108199,0.205678135964346,
0.90431621462679));
#30311=CARTESIAN_POINT('Ctrl Pts',(-0.059434718443707,0.19738583763708,
0.908022428621162));
#30312=CARTESIAN_POINT('Ctrl Pts',(-0.112405647662483,0.160223891616111,
0.911728642615534));
#30313=CARTESIAN_POINT('Ctrl Pts',(-0.163307724594775,0.124513356361944,
0.915290105339548));
#30314=CARTESIAN_POINT('Ctrl Pts',(-0.195507366281261,0.0621442230158499,
0.918851568063562));
#30315=CARTESIAN_POINT('Ctrl Pts',(-0.195707453392556,-4.66568259871601E-5,
0.922413030787576));
#30316=CARTESIAN_POINT('Origin',(0.,0.,0.));
#30317=CARTESIAN_POINT('',(-0.195268202714777,0.000165579016441021,1.00258696921242));
#30318=CARTESIAN_POINT('',(-0.19535343393295,0.000178280253715055,0.992413030787576));
#30319=CARTESIAN_POINT('',(-0.1954,-2.39295984553393E-17,0.));
#30320=CARTESIAN_POINT('Ctrl Pts',(-0.195268202714777,0.000165579016441021,
1.00258696921242));
#30321=CARTESIAN_POINT('Ctrl Pts',(-0.19542709496717,0.0198793394721131,
1.00146457155455));
#30322=CARTESIAN_POINT('Ctrl Pts',(-0.192681564478375,0.0395498739780043,
1.00034217389668));
#30323=CARTESIAN_POINT('Ctrl Pts',(-0.186848643290836,0.0582577638715851,
0.999219776238813));
#30324=CARTESIAN_POINT('Ctrl Pts',(-0.167600993827966,0.11999062383733,
0.995516054555966));
#30325=CARTESIAN_POINT('Ctrl Pts',(-0.114735119634562,0.171241362792136,
0.991812332873117));
#30326=CARTESIAN_POINT('Ctrl Pts',(-0.0524351231736321,0.18856531990772,
0.988108611190269));
#30327=CARTESIAN_POINT('Ctrl Pts',(0.00986487328729629,0.205889277023303,
0.984404889507421));
#30328=CARTESIAN_POINT('Ctrl Pts',(0.0815989920157509,0.189286452299667,
0.980701167824573));
#30329=CARTESIAN_POINT('Ctrl Pts',(0.129952003507049,0.146351732792493,
0.976997446141725));
#30330=CARTESIAN_POINT('Ctrl Pts',(0.178305014998348,0.103417013285319,
0.973293724458878));
#30331=CARTESIAN_POINT('Ctrl Pts',(0.20327691925249,0.0341503989946047,
0.969590002776029));
#30332=CARTESIAN_POINT('Ctrl Pts',(0.19344406978275,-0.0297614493697593,
0.965886281093181));
#30333=CARTESIAN_POINT('Ctrl Pts',(0.18361122031301,-0.0936732977341234,
0.962182559410334));
#30334=CARTESIAN_POINT('Ctrl Pts',(0.138973617119388,-0.152230380172138,
0.958478837727486));
#30335=CARTESIAN_POINT('Ctrl Pts',(0.0799511084736072,-0.178645358874384,
0.954775116044638));
#30336=CARTESIAN_POINT('Ctrl Pts',(0.0209285998278261,-0.20506033757663,
0.95107139436179));
#30337=CARTESIAN_POINT('Ctrl Pts',(-0.0524788142701144,-0.199333212543108,
0.947367672678942));
#30338=CARTESIAN_POINT('Ctrl Pts',(-0.106690354347858,-0.16408387214268,
0.943663950996094));
#30339=CARTESIAN_POINT('Ctrl Pts',(-0.160735113766186,-0.128942975594381,
0.93997162373487));
#30340=CARTESIAN_POINT('Ctrl Pts',(-0.195701928883641,-0.0644612332051665,
0.936279296473647));
#30341=CARTESIAN_POINT('Ctrl Pts',(-0.195719986784682,3.71606954582295E-6,
0.932586969212424));
#30342=CARTESIAN_POINT('Ctrl Pts',(-0.195707453392556,-4.66568259871601E-5,
0.922413030787576));
#30343=CARTESIAN_POINT('Ctrl Pts',(-0.195715585687005,-0.00257432861687418,
0.922557782057934));
#30344=CARTESIAN_POINT('Ctrl Pts',(-0.195670857405051,-0.00510170594794435,
0.922702533328292));
#30345=CARTESIAN_POINT('Ctrl Pts',(-0.195572375776859,-0.00762698699047084,
0.92284728459865));
#30346=CARTESIAN_POINT('Ctrl Pts',(-0.193050850489432,-0.0722843258614067,
0.926553498593022));
#30347=CARTESIAN_POINT('Ctrl Pts',(-0.155290475731554,-0.135567409888606,
0.930259712587394));
#30348=CARTESIAN_POINT('Ctrl Pts',(-0.0995863227266852,-0.168491214354887,
0.933965926581766));
#30349=CARTESIAN_POINT('Ctrl Pts',(-0.0438821697218168,-0.201415018821168,
0.937672140576139));
#30350=CARTESIAN_POINT('Ctrl Pts',(0.0297657615300397,-0.203979543726533,
0.94137835457051));
#30351=CARTESIAN_POINT('Ctrl Pts',(0.0876251218790847,-0.175010180082627,
0.945084568564882));
#30352=CARTESIAN_POINT('Ctrl Pts',(0.145484482228131,-0.146040816438721,
0.948790782559255));
#30353=CARTESIAN_POINT('Ctrl Pts',(0.187555271674363,-0.0855375642455424,
0.952496996553627));
#30354=CARTESIAN_POINT('Ctrl Pts',(0.194568154283725,-0.021212227253196,
0.956203210547999));
#30355=CARTESIAN_POINT('Ctrl Pts',(0.201581036893087,0.0431131097391505,
0.959909424542371));
#30356=CARTESIAN_POINT('Ctrl Pts',(0.173536012665579,0.111260531530666,
0.963615638536743));
#30357=CARTESIAN_POINT('Ctrl Pts',(0.123278314419194,0.152017044141902,
0.967321852531115));
#30358=CARTESIAN_POINT('Ctrl Pts',(0.0730206161728088,0.192773556753138,
0.971028066525487));
#30359=CARTESIAN_POINT('Ctrl Pts',(0.000550243907548716,0.206139160184095,
0.974734280519859));
#30360=CARTESIAN_POINT('Ctrl Pts',(-0.0609398062732146,0.185992111567971,
0.978440494514231));
#30361=CARTESIAN_POINT('Ctrl Pts',(-0.122429856453979,0.165845062951848,
0.982146708508603));
#30362=CARTESIAN_POINT('Ctrl Pts',(-0.172939584550245,0.112185362288641,
0.985852922502976));
#30363=CARTESIAN_POINT('Ctrl Pts',(-0.189334427223443,0.0495903289718102,
0.989559136497348));
#30364=CARTESIAN_POINT('Ctrl Pts',(-0.193542598326109,0.0335236538822793,
0.990510434594091));
#30365=CARTESIAN_POINT('Ctrl Pts',(-0.195503184094814,0.0168682937546108,
0.991461732690834));
#30366=CARTESIAN_POINT('Ctrl Pts',(-0.19535343393295,0.000178280253715055,
0.992413030787576));
#30367=CARTESIAN_POINT('Origin',(0.,0.,0.));
#30368=CARTESIAN_POINT('',(-0.195129684289216,-0.000113636086278679,1.07258696921242));
#30369=CARTESIAN_POINT('',(-0.195093054978418,-5.50606481354719E-5,1.06241303078758));
#30370=CARTESIAN_POINT('',(-0.1954,-2.39295984553393E-17,0.));
#30371=CARTESIAN_POINT('Ctrl Pts',(-0.195129684289216,-0.000113636086278679,
1.07258696921242));
#30372=CARTESIAN_POINT('Ctrl Pts',(-0.194942963316978,0.0391854106201406,
1.07035356831831));
#30373=CARTESIAN_POINT('Ctrl Pts',(-0.183442754086643,0.0785903964976412,
1.06812016742419));
#30374=CARTESIAN_POINT('Ctrl Pts',(-0.161381630858742,0.110744756631717,
1.06588676653008));
#30375=CARTESIAN_POINT('Ctrl Pts',(-0.124796949325566,0.164067382739912,
1.06218304484723));
#30376=CARTESIAN_POINT('Ctrl Pts',(-0.0591690439027595,0.197450300329055,
1.05847932316438));
#30377=CARTESIAN_POINT('Ctrl Pts',(0.00547076636758263,0.195640786233593,
1.05477560148153));
#30378=CARTESIAN_POINT('Ctrl Pts',(0.0701105766379276,0.19383127213813,
1.05107187979868));
#30379=CARTESIAN_POINT('Ctrl Pts',(0.133762291755807,0.156829326358058,
1.04736815811584));
#30380=CARTESIAN_POINT('Ctrl Pts',(0.167312833478204,0.101552035674769,
1.04366443643299));
#30381=CARTESIAN_POINT('Ctrl Pts',(0.200863375200599,0.0462747449914819,
1.03996071475014));
#30382=CARTESIAN_POINT('Ctrl Pts',(0.204312743527515,-0.0272778905950186,
1.03625699306729));
#30383=CARTESIAN_POINT('Ctrl Pts',(0.17608042651717,-0.0854535269464722,
1.03255327138444));
#30384=CARTESIAN_POINT('Ctrl Pts',(0.147848109506825,-0.143629163297926,
1.0288495497016));
#30385=CARTESIAN_POINT('Ctrl Pts',(0.0879341071592168,-0.186427800414334,
1.02514582801875));
#30386=CARTESIAN_POINT('Ctrl Pts',(0.0237478981470821,-0.194273555725334,
1.0214421063359));
#30387=CARTESIAN_POINT('Ctrl Pts',(-0.0404383108650536,-0.202119311036335,
1.01773838465305));
#30388=CARTESIAN_POINT('Ctrl Pts',(-0.108896726541717,-0.175012184541928,
1.0140346629702));
#30389=CARTESIAN_POINT('Ctrl Pts',(-0.15031122201388,-0.125351130806383,
1.01033094128736));
#30390=CARTESIAN_POINT('Ctrl Pts',(-0.17917522457641,-0.0907396556226723,
1.00774961726238));
#30391=CARTESIAN_POINT('Ctrl Pts',(-0.194902777514884,-0.0451727225472274,
1.0051682932374));
#30392=CARTESIAN_POINT('Ctrl Pts',(-0.195268202714777,0.000165579016441021,
1.00258696921242));
#30393=CARTESIAN_POINT('Ctrl Pts',(-0.19535343393295,0.000178280253715055,
0.992413030787576));
#30394=CARTESIAN_POINT('Ctrl Pts',(-0.194919764294582,-0.0481552375812319,
0.995167946685205));
#30395=CARTESIAN_POINT('Ctrl Pts',(-0.176787653021499,-0.0967793777264111,
0.997922862582834));
#30396=CARTESIAN_POINT('Ctrl Pts',(-0.144290486192301,-0.132238333502052,
1.00067777848046));
#30397=CARTESIAN_POINT('Ctrl Pts',(-0.100571745237828,-0.179941596688631,
1.00438399247484));
#30398=CARTESIAN_POINT('Ctrl Pts',(-0.0308543060787511,-0.203817757091334,
1.00809020646921));
#30399=CARTESIAN_POINT('Ctrl Pts',(0.0329297761185238,-0.192930969998698,
1.01179642046358));
#30400=CARTESIAN_POINT('Ctrl Pts',(0.0967138583157977,-0.182044182906063,
1.01550263445795));
#30401=CARTESIAN_POINT('Ctrl Pts',(0.15456458355127,-0.136394448318089,
1.01920884845232));
#30402=CARTESIAN_POINT('Ctrl Pts',(0.179984980484802,-0.076890421197536,
1.0229150624467));
#30403=CARTESIAN_POINT('Ctrl Pts',(0.205405377418334,-0.0173863940769825,
1.02662127644107));
#30404=CARTESIAN_POINT('Ctrl Pts',(0.198395446049928,0.05597192557615,1.03032749043544));
#30405=CARTESIAN_POINT('Ctrl Pts',(0.162166047466929,0.109585000349956,
1.03403370442981));
#30406=CARTESIAN_POINT('Ctrl Pts',(0.12593664888393,0.163198075123761,1.03773991842419));
#30407=CARTESIAN_POINT('Ctrl Pts',(0.0604877830863377,0.19706590501824,
1.04144613241856));
#30408=CARTESIAN_POINT('Ctrl Pts',(-0.0042038551539475,0.195675976549601,
1.04515234641293));
#30409=CARTESIAN_POINT('Ctrl Pts',(-0.0688954933942345,0.194286048080962,
1.0488585604073));
#30410=CARTESIAN_POINT('Ctrl Pts',(-0.132829904077215,0.157638361249205,
1.05256477440167));
#30411=CARTESIAN_POINT('Ctrl Pts',(-0.166723158702796,0.102518946943711,
1.05627098839605));
#30412=CARTESIAN_POINT('Ctrl Pts',(-0.185446111291195,0.0720704641366568,
1.05831833585989));
#30413=CARTESIAN_POINT('Ctrl Pts',(-0.195001820365716,0.0359852200961074,
1.06036568332373));
#30414=CARTESIAN_POINT('Ctrl Pts',(-0.195093054978418,-5.50606481354719E-5,
1.06241303078758));
#30415=CARTESIAN_POINT('Origin',(0.,0.,-0.129405622560369));
#30416=CARTESIAN_POINT('',(-0.155334812646815,-9.04610707407963E-5,1.09559437743963));
#30417=CARTESIAN_POINT('',(-0.155659711405804,-0.000105088068675666,1.10940562256037));
#30418=CARTESIAN_POINT('',(-0.15555,-2.01987159101623E-14,-0.129405622560369));
#30419=CARTESIAN_POINT('',(0.0499806597877791,0.147301514408978,1.14445));
#30420=CARTESIAN_POINT('Ctrl Pts',(-0.155334812646815,-9.04610707408108E-5,
1.09559437743963));
#30421=CARTESIAN_POINT('Ctrl Pts',(-0.155432667860164,-0.0206859868644216,
1.09706469822836));
#30422=CARTESIAN_POINT('Ctrl Pts',(-0.142041322258558,-0.0930327919713715,
1.10223874069994));
#30423=CARTESIAN_POINT('Ctrl Pts',(-0.0324962964057439,-0.180887727526569,
1.11111650485437));
#30424=CARTESIAN_POINT('Ctrl Pts',(0.134445241673909,-0.125560970886474,
1.12222766990291));
#30425=CARTESIAN_POINT('Ctrl Pts',(0.178171768593789,0.0450698535437549,
1.13333883495146));
#30426=CARTESIAN_POINT('Ctrl Pts',(0.0989503531151977,0.130685679928735,
1.14074627831715));
#30427=CARTESIAN_POINT('Ctrl Pts',(0.0499806597877626,0.147301514408983,
1.14445));
#30428=CARTESIAN_POINT('',(0.155548765964692,0.000619602180124784,1.14445));
#30429=CARTESIAN_POINT('Origin',(0.,0.,1.14445));
#30430=CARTESIAN_POINT('Ctrl Pts',(-0.155659711405804,-0.00010508806867568,
1.10940562256037));
#30431=CARTESIAN_POINT('Ctrl Pts',(-0.155726922058417,-0.0079449137192624,
1.1099684397238));
#30432=CARTESIAN_POINT('Ctrl Pts',(-0.151630179095532,-0.0673453815214831,
1.1142374708816));
#30433=CARTESIAN_POINT('Ctrl Pts',(-0.075277483453787,-0.167898453189698,
1.12221271603377));
#30434=CARTESIAN_POINT('Ctrl Pts',(0.100462758039806,-0.153944373403644,
1.13333135801688));
#30435=CARTESIAN_POINT('Ctrl Pts',(0.155754888396286,-0.0511266487217653,
1.14074378600563));
#30436=CARTESIAN_POINT('Ctrl Pts',(0.155548765964692,0.000619602180124784,
1.14445));
#30437=CARTESIAN_POINT('Origin',(0.,0.,-0.129405622560369));
#30438=CARTESIAN_POINT('',(-0.155445081536763,0.000131810726739325,1.02559437743963));
#30439=CARTESIAN_POINT('',(-0.155305653540906,-4.38315446397164E-5,1.03940562256037));
#30440=CARTESIAN_POINT('',(-0.15555,-2.01987159101623E-14,-0.129405622560369));
#30441=CARTESIAN_POINT('Ctrl Pts',(-0.155445081536763,0.000131810726739319,
1.02559437743963));
#30442=CARTESIAN_POINT('Ctrl Pts',(-0.155154181384031,-0.0359601688445403,
1.02817570146461));
#30443=CARTESIAN_POINT('Ctrl Pts',(-0.124670140973274,-0.124280598265434,
1.03446074717243));
#30444=CARTESIAN_POINT('Ctrl Pts',(0.0223056668548975,-0.182477852394609,
1.04444951456311));
#30445=CARTESIAN_POINT('Ctrl Pts',(0.165390974917898,-0.0802670846854376,
1.05556067961165));
#30446=CARTESIAN_POINT('Ctrl Pts',(0.157153269033781,0.0953897085409752,
1.06667184466019));
#30447=CARTESIAN_POINT('Ctrl Pts',(0.00514163720288116,0.183756944970195,
1.07778300970874));
#30448=CARTESIAN_POINT('Ctrl Pts',(-0.130849536725084,0.114582374749785,
1.08742385396855));
#30449=CARTESIAN_POINT('Ctrl Pts',(-0.155186171668149,0.0311939131113674,
1.09336097654551));
#30450=CARTESIAN_POINT('Ctrl Pts',(-0.155334812646815,-9.04610707408108E-5,
1.09559437743963));
#30451=CARTESIAN_POINT('Ctrl Pts',(-0.155305653540906,-4.38315446397077E-5,
1.03940562256037));
#30452=CARTESIAN_POINT('Ctrl Pts',(-0.155364500629154,-0.0232901140548306,
1.0410644890909));
#30453=CARTESIAN_POINT('Ctrl Pts',(-0.139557528484751,-0.0983968830408974,
1.0464295696158));
#30454=CARTESIAN_POINT('Ctrl Pts',(-0.0231259578302998,-0.182421227428175,
1.05550086413507));
#30455=CARTESIAN_POINT('Ctrl Pts',(0.140774638007895,-0.11829694620695,
1.06661950611819));
#30456=CARTESIAN_POINT('Ctrl Pts',(0.175706993010233,0.0541796064983141,
1.07773814810131));
#30457=CARTESIAN_POINT('Ctrl Pts',(0.0497080432048737,0.177049779856472,
1.08885679008442));
#30458=CARTESIAN_POINT('Ctrl Pts',(-0.113185991314487,0.139680492671116,
1.09941261490411));
#30459=CARTESIAN_POINT('Ctrl Pts',(-0.155284332390808,0.0436812153822664,
1.10626222572943));
#30460=CARTESIAN_POINT('Ctrl Pts',(-0.155659711405804,-0.00010508806867568,
1.10940562256037));
#30461=CARTESIAN_POINT('Origin',(0.,0.,-0.129405622560369));
#30462=CARTESIAN_POINT('',(-0.155804728476752,2.95821195149996E-6,0.95559437743963));
#30463=CARTESIAN_POINT('',(-0.155512930646214,0.000141921665610299,0.969405622560371));
#30464=CARTESIAN_POINT('',(-0.15555,-2.01987159101623E-14,-0.129405622560369));
#30465=CARTESIAN_POINT('Ctrl Pts',(-0.155804728476752,2.95821195150548E-6,
0.95559437743963));
#30466=CARTESIAN_POINT('Ctrl Pts',(-0.155790353315504,-0.0513149683984934,
0.959286704700854));
#30467=CARTESIAN_POINT('Ctrl Pts',(-0.100033131917675,-0.154135965233235,
0.966682753644926));
#30468=CARTESIAN_POINT('Ctrl Pts',(0.0750970673805211,-0.167799333720618,
0.977782524271844));
#30469=CARTESIAN_POINT('Ctrl Pts',(0.181699613594968,-0.0279545920640164,
0.988893689320389));
#30470=CARTESIAN_POINT('Ctrl Pts',(0.122062258834496,0.137466418983892,
1.00000485436893));
#30471=CARTESIAN_POINT('Ctrl Pts',(-0.0492515922639386,0.177116921324136,
1.01111601941748));
#30472=CARTESIAN_POINT('Ctrl Pts',(-0.146173837715872,0.0831558022400444,
1.01964586044104));
#30473=CARTESIAN_POINT('Ctrl Pts',(-0.155571569202373,0.015825134364817,
1.02447197978176));
#30474=CARTESIAN_POINT('Ctrl Pts',(-0.155445081536763,0.000131810726739319,
1.02559437743963));
#30475=CARTESIAN_POINT('Ctrl Pts',(-0.155512930646214,0.000141921665610296,
0.969405622560371));
#30476=CARTESIAN_POINT('Ctrl Pts',(-0.155167703869094,-0.0383344278698275,
0.972160538458));
#30477=CARTESIAN_POINT('Ctrl Pts',(-0.121314953523015,-0.129115961930375,
0.97862166835));
#30478=CARTESIAN_POINT('Ctrl Pts',(0.0309373610575528,-0.181257875466721,
0.988789012236375));
#30479=CARTESIAN_POINT('Ctrl Pts',(0.169095195914933,-0.0722381792257861,
0.999907654219489));
#30480=CARTESIAN_POINT('Ctrl Pts',(0.152354231364944,0.102954552944809,
1.01102629620261));
#30481=CARTESIAN_POINT('Ctrl Pts',(-0.00394931635484403,0.183836962465064,
1.02214493818572));
#30482=CARTESIAN_POINT('Ctrl Pts',(-0.133855689695156,0.109373648628768,
1.03160471363831));
#30483=CARTESIAN_POINT('Ctrl Pts',(-0.15523302537302,0.0286463714736223,
1.03735827509653));
#30484=CARTESIAN_POINT('Ctrl Pts',(-0.155305653540906,-4.38315446397077E-5,
1.03940562256037));
#30485=CARTESIAN_POINT('Origin',(0.,0.,-0.129405622560369));
#30486=CARTESIAN_POINT('',(-0.155453687436568,-0.000133745576774406,0.885594377439631));
#30487=CARTESIAN_POINT('',(-0.155794751152569,-3.71416033132788E-5,0.899405622560372));
#30488=CARTESIAN_POINT('',(-0.15555,-2.01987159101623E-14,-0.129405622560369));
#30489=CARTESIAN_POINT('Ctrl Pts',(-0.155453687436568,-0.000133745576774402,
0.885594377439631));
#30490=CARTESIAN_POINT('Ctrl Pts',(-0.155579877499581,-0.0155062375664632,
0.886693986254252));
#30491=CARTESIAN_POINT('Ctrl Pts',(-0.146423861786649,-0.0825096309536398,
0.891497316751722));
#30492=CARTESIAN_POINT('Ctrl Pts',(-0.0503376402892206,-0.17681153483915,
0.900004368932038));
#30493=CARTESIAN_POINT('Ctrl Pts',(0.12121644264892,-0.138212772940753,
0.911115533980582));
#30494=CARTESIAN_POINT('Ctrl Pts',(0.181867711471885,0.026839009932345,
0.922226699029127));
#30495=CARTESIAN_POINT('Ctrl Pts',(0.0761253709552246,0.167335367481701,
0.933337864077668));
#30496=CARTESIAN_POINT('Ctrl Pts',(-0.099265255914171,0.154733978795034,
0.944449029126215));
#30497=CARTESIAN_POINT('Ctrl Pts',(-0.155732851093913,0.0517959404958592,
0.951867866913534));
#30498=CARTESIAN_POINT('Ctrl Pts',(-0.155804772838109,0.000161323939398619,
0.955582983018006));
#30499=CARTESIAN_POINT('Ctrl Pts',(-0.155804728476752,2.95821195150548E-6,
0.95559437743963));
#30500=CARTESIAN_POINT('Ctrl Pts',(-0.155794751152569,-3.71416033132616E-5,
0.899405622560372));
#30501=CARTESIAN_POINT('Ctrl Pts',(-0.155801224941728,-0.0020493184051098,
0.899550373830729));
#30502=CARTESIAN_POINT('Ctrl Pts',(-0.154853952527048,-0.055575068168544,
0.903401339095459));
#30503=CARTESIAN_POINT('Ctrl Pts',(-0.0935609375970031,-0.15829679799695,
0.91095851835456));
#30504=CARTESIAN_POINT('Ctrl Pts',(0.0823234386500799,-0.164421340203127,
0.922077160337675));
#30505=CARTESIAN_POINT('Ctrl Pts',(0.182795976495949,-0.0199287985657338,
0.933195802320793));
#30506=CARTESIAN_POINT('Ctrl Pts',(0.115819463928053,0.142819381470141,
0.944314444303908));
#30507=CARTESIAN_POINT('Ctrl Pts',(-0.0572526917402423,0.174738822826618,
0.955433086287024));
#30508=CARTESIAN_POINT('Ctrl Pts',(-0.147990815776177,0.0783419353749631,
0.963796812372513));
#30509=CARTESIAN_POINT('Ctrl Pts',(-0.15563214066504,0.01342816322173,0.968454324463628));
#30510=CARTESIAN_POINT('Ctrl Pts',(-0.155512930646214,0.000141921665610296,
0.969405622560371));
#30511=CARTESIAN_POINT('Origin',(0.,0.,-0.129405622560369));
#30512=CARTESIAN_POINT('',(-0.155333906144275,7.80263919018194E-5,0.815594377439631));
#30513=CARTESIAN_POINT('',(-0.155403083159801,-0.000119596074553197,0.829405622560371));
#30514=CARTESIAN_POINT('',(-0.15555,-2.01987159101623E-14,-0.129405622560369));
#30515=CARTESIAN_POINT('Ctrl Pts',(-0.155333906144275,7.80263919018167E-5,
0.815594377439631));
#30516=CARTESIAN_POINT('Ctrl Pts',(-0.155193217426013,-0.0308862600127516,
0.817804989490498));
#30517=CARTESIAN_POINT('Ctrl Pts',(-0.13122308335565,-0.113929638534857,
0.823719323224213));
#30518=CARTESIAN_POINT('Ctrl Pts',(0.00400949547363229,-0.183793690702293,
0.833337378640777));
#30519=CARTESIAN_POINT('Ctrl Pts',(0.156567267939011,-0.0963477420579929,
0.844448543689319));
#30520=CARTESIAN_POINT('Ctrl Pts',(0.165879203582308,0.0792482593671729,
0.855559708737864));
#30521=CARTESIAN_POINT('Ctrl Pts',(0.0234256671005791,0.182338791618694,
0.866670873786407));
#30522=CARTESIAN_POINT('Ctrl Pts',(-0.124241507899534,0.124912116508194,
0.87668243002033));
#30523=CARTESIAN_POINT('Ctrl Pts',(-0.155154841917538,0.0362716593952071,
0.882990264571404));
#30524=CARTESIAN_POINT('Ctrl Pts',(-0.155453687436568,-0.000133745576774402,
0.885594377439631));
#30525=CARTESIAN_POINT('Ctrl Pts',(-0.155403083159801,-0.000119596074553188,
0.829405622560371));
#30526=CARTESIAN_POINT('Ctrl Pts',(-0.155527408252746,-0.017480188940304,
0.830646423197829));
#30527=CARTESIAN_POINT('Ctrl Pts',(-0.14483135129372,-0.0865473027753662,
0.83559343782966));
#30528=CARTESIAN_POINT('Ctrl Pts',(-0.0434704832044991,-0.178666848096071,
0.844246666455862));
#30529=CARTESIAN_POINT('Ctrl Pts',(0.126590215885116,-0.133365823077974,
0.855365308438979));
#30530=CARTESIAN_POINT('Ctrl Pts',(0.18068878531032,0.0341040818691465,
0.866483950422094));
#30531=CARTESIAN_POINT('Ctrl Pts',(0.069268588294083,0.170333168137465,
0.877602592405212));
#30532=CARTESIAN_POINT('Ctrl Pts',(-0.103328002592178,0.150787500329959,
0.888576483117969));
#30533=CARTESIAN_POINT('Ctrl Pts',(-0.155635469933735,0.0494704907375218,
0.895844159836357));
#30534=CARTESIAN_POINT('Ctrl Pts',(-0.155794751152569,-3.71416033132616E-5,
0.899405622560372));
#30535=CARTESIAN_POINT('Origin',(0.,0.,-0.129405622560369));
#30536=CARTESIAN_POINT('',(-0.155738164088485,9.0367155389158E-5,0.745594377439631));
#30537=CARTESIAN_POINT('',(-0.155363820104426,0.000100737127591941,0.759405622560371));
#30538=CARTESIAN_POINT('',(-0.15555,-2.01987159101623E-14,-0.129405622560369));
#30539=CARTESIAN_POINT('Ctrl Pts',(-0.155738164088485,9.03671553891608E-5,
0.745594377439631));
#30540=CARTESIAN_POINT('Ctrl Pts',(-0.155418612064456,-0.0461276292775272,
0.748915992726744));
#30541=CARTESIAN_POINT('Ctrl Pts',(-0.109121796390773,-0.144436334125619,
0.755941329696705));
#30542=CARTESIAN_POINT('Ctrl Pts',(0.0580004387659595,-0.174448118065669,
0.766670388349515));
#30543=CARTESIAN_POINT('Ctrl Pts',(0.17800908511122,-0.0459234407622611,
0.777781553398057));
#30544=CARTESIAN_POINT('Ctrl Pts',(0.135154441460109,0.124617309179735,
0.788892718446602));
#30545=CARTESIAN_POINT('Ctrl Pts',(-0.0313551099181417,0.181143738163968,
0.800003883495145));
#30546=CARTESIAN_POINT('Ctrl Pts',(-0.141757073229054,0.0936656796997624,
0.808904436492822));
#30547=CARTESIAN_POINT('Ctrl Pts',(-0.155428931266511,0.0209921774117757,
0.81410126780765));
#30548=CARTESIAN_POINT('Ctrl Pts',(-0.155333906144275,7.80263919018167E-5,
0.815594377439631));
#30549=CARTESIAN_POINT('Ctrl Pts',(-0.155363820104426,0.000100737127591942,
0.759405622560371));
#30550=CARTESIAN_POINT('Ctrl Pts',(-0.155169765832855,-0.0326159426902871,
0.76174247256493));
#30551=CARTESIAN_POINT('Ctrl Pts',(-0.129071878250434,-0.117503987929593,
0.767785536563862));
#30552=CARTESIAN_POINT('Ctrl Pts',(0.0103792628149562,-0.18358593744105,
0.777534814557165));
#30553=CARTESIAN_POINT('Ctrl Pts',(0.159909575810308,-0.0907769413831382,
0.78865345654028));
#30554=CARTESIAN_POINT('Ctrl Pts',(0.162955779866738,0.0851876712390422,
0.799772098523398));
#30555=CARTESIAN_POINT('Ctrl Pts',(0.0167274199086701,0.183116681231986,
0.810890740506512));
#30556=CARTESIAN_POINT('Ctrl Pts',(-0.126795424285233,0.121093838634352,
0.820768581852172));
#30557=CARTESIAN_POINT('Ctrl Pts',(-0.155156054962447,0.0343750973057136,
0.826940209203457));
#30558=CARTESIAN_POINT('Ctrl Pts',(-0.155403083159801,-0.000119596074553188,
0.829405622560371));
#30559=CARTESIAN_POINT('Origin',(0.,0.,-0.129405622560369));
#30560=CARTESIAN_POINT('',(-0.155606466149984,-0.000136591087330588,0.67559437743963));
#30561=CARTESIAN_POINT('',(-0.155769406638298,6.77585252333857E-5,0.689405622560371));
#30562=CARTESIAN_POINT('',(-0.15555,-2.01987159101623E-14,-0.129405622560369));
#30563=CARTESIAN_POINT('Ctrl Pts',(-0.155606466149984,-0.000136591087330577,
0.67559437743963));
#30564=CARTESIAN_POINT('Ctrl Pts',(-0.155699698050756,-0.010301028373747,
0.676323274280142));
#30565=CARTESIAN_POINT('Ctrl Pts',(-0.150160999329305,-0.0720125819190329,
0.680755892803501));
#30566=CARTESIAN_POINT('Ctrl Pts',(-0.0677079673289082,-0.170914680334463,
0.68889223300971));
#30567=CARTESIAN_POINT('Ctrl Pts',(0.106838781720774,-0.149605051766532,
0.700003398058251));
#30568=CARTESIAN_POINT('Ctrl Pts',(0.183637062036826,0.00858057341481814,
0.711114563106797));
#30569=CARTESIAN_POINT('Ctrl Pts',(0.0924229284360449,0.1589156980696,0.722225728155339));
#30570=CARTESIAN_POINT('Ctrl Pts',(-0.0833503847528551,0.163856370505402,
0.733336893203883));
#30571=CARTESIAN_POINT('Ctrl Pts',(-0.153115801604342,0.0622214122864029,
0.741126442965314));
#30572=CARTESIAN_POINT('Ctrl Pts',(-0.155774924177056,0.00540711533618156,
0.745212271043896));
#30573=CARTESIAN_POINT('Ctrl Pts',(-0.155738164088485,9.03671553891608E-5,
0.745594377439631));
#30574=CARTESIAN_POINT('Ctrl Pts',(-0.155769406638298,6.77585252333878E-5,
0.689405622560371));
#30575=CARTESIAN_POINT('Ctrl Pts',(-0.155508734647919,-0.0476733936548398,
0.692838521932031));
#30576=CARTESIAN_POINT('Ctrl Pts',(-0.106472330039144,-0.147419539900055,
0.699977635298063));
#30577=CARTESIAN_POINT('Ctrl Pts',(0.0633314188332071,-0.172628667698419,
0.710822962658467));
#30578=CARTESIAN_POINT('Ctrl Pts',(0.17940008868909,-0.0403377453646542,
0.721941604641583));
#30579=CARTESIAN_POINT('Ctrl Pts',(0.131130494233742,0.128904301731096,
0.733060246624699));
#30580=CARTESIAN_POINT('Ctrl Pts',(-0.0372603218894873,0.180064416072257,
0.744178888607816));
#30581=CARTESIAN_POINT('Ctrl Pts',(-0.143301362666466,0.0901927254173143,
0.752960680586373));
#30582=CARTESIAN_POINT('Ctrl Pts',(-0.155477533406966,0.0192722899107996,
0.758036258570558));
#30583=CARTESIAN_POINT('Ctrl Pts',(-0.155363820104426,0.000100737127591942,
0.759405622560371));
#30584=CARTESIAN_POINT('Origin',(0.,0.,-0.129405622560369));
#30585=CARTESIAN_POINT('',(-0.155295085115974,-2.74912889200857E-6,0.60559437743963));
#30586=CARTESIAN_POINT('',(-0.155567057787938,-0.000141549514015751,0.619405622560371));
#30587=CARTESIAN_POINT('',(-0.15555,-2.01987159101623E-14,-0.129405622560369));
#30588=CARTESIAN_POINT('Ctrl Pts',(-0.155295114066544,-2.74881667468134E-6,
0.60559437743963));
#30589=CARTESIAN_POINT('Ctrl Pts',(-0.155299180574127,-0.0257905198155464,
0.607434277516388));
#30590=CARTESIAN_POINT('Ctrl Pts',(-0.137005956536857,-0.103483686203599,
0.612977899275993));
#30591=CARTESIAN_POINT('Ctrl Pts',(-0.0143272298638598,-0.183278278249422,
0.622225242718446));
#30592=CARTESIAN_POINT('Ctrl Pts',(0.146185859526926,-0.111471481859797,
0.63333640776699));
#30593=CARTESIAN_POINT('Ctrl Pts',(0.172951224644592,0.0623223129190563,
0.644447572815534));
#30594=CARTESIAN_POINT('Ctrl Pts',(0.0414808152398764,0.179096450999678,
0.655558737864077));
#30595=CARTESIAN_POINT('Ctrl Pts',(-0.11682689842466,0.135101180160119,
0.66594100607211));
#30596=CARTESIAN_POINT('Ctrl Pts',(-0.155225961585962,0.0413472223515983,
0.672619552597294));
#30597=CARTESIAN_POINT('Ctrl Pts',(-0.155606466149984,-0.000136591087330577,
0.67559437743963));
#30598=CARTESIAN_POINT('Ctrl Pts',(-0.155567057787938,-0.000141549514015748,
0.619405622560371));
#30599=CARTESIAN_POINT('Ctrl Pts',(-0.155673152840384,-0.011622012238534,
0.62022835730476));
#30600=CARTESIAN_POINT('Ctrl Pts',(-0.149271086742403,-0.0747018195902368,
0.62475730604352));
#30601=CARTESIAN_POINT('Ctrl Pts',(-0.0632665469493242,-0.172652453095426,
0.632992468776653));
#30602=CARTESIAN_POINT('Ctrl Pts',(0.110806726459172,-0.146742614445027,
0.644111110759769));
#30603=CARTESIAN_POINT('Ctrl Pts',(0.183376231205259,0.0135898253011021,
0.655229752742886));
#30604=CARTESIAN_POINT('Ctrl Pts',(0.0879651525947856,0.161473395492061,
0.666348394726001));
#30605=CARTESIAN_POINT('Ctrl Pts',(-0.0880258220622017,0.161440330069759,
0.677467036709119));
#30606=CARTESIAN_POINT('Ctrl Pts',(-0.153940153309356,0.0591912849892102,
0.685152779320574));
#30607=CARTESIAN_POINT('Ctrl Pts',(-0.155790160368306,0.00386873070159844,
0.689132307937659));
#30608=CARTESIAN_POINT('Ctrl Pts',(-0.155769406638298,6.77585252333878E-5,
0.689405622560371));
#30609=CARTESIAN_POINT('Origin',(0.,0.,-0.129405622560369));
#30610=CARTESIAN_POINT('',(-0.155596383579478,0.000138071545366175,0.53559437743963));
#30611=CARTESIAN_POINT('',(-0.15529563387483,1.51106445085702E-5,0.549405622560371));
#30612=CARTESIAN_POINT('',(-0.15555,-2.01987159101623E-14,-0.129405622560369));
#30613=CARTESIAN_POINT('Ctrl Pts',(-0.155596383579478,0.000138071545366179,
0.53559437743963));
#30614=CARTESIAN_POINT('Ctrl Pts',(-0.155217514150148,-0.0410190199764792,
0.538545280752634));
#30615=CARTESIAN_POINT('Ctrl Pts',(-0.117330640529453,-0.134449549172498,
0.545199905748485));
#30616=CARTESIAN_POINT('Ctrl Pts',(0.0403262995152723,-0.179359935217008,
0.555558252427184));
#30617=CARTESIAN_POINT('Ctrl Pts',(0.172546185411942,-0.0634350903950841,
0.566669417475728));
#30618=CARTESIAN_POINT('Ctrl Pts',(0.146900873501267,0.11052750860401,0.577780582524271));
#30619=CARTESIAN_POINT('Ctrl Pts',(-0.013146340126236,0.183366765077345,
0.588891747572816));
#30620=CARTESIAN_POINT('Ctrl Pts',(-0.136655195880861,0.104159698732297,
0.598163012544601));
#30621=CARTESIAN_POINT('Ctrl Pts',(-0.155290994688111,0.0261203028467153,
0.60373055583354));
#30622=CARTESIAN_POINT('Ctrl Pts',(-0.155295114066544,-2.74881667468134E-6,
0.60559437743963));
#30623=CARTESIAN_POINT('Ctrl Pts',(-0.15529563387483,1.51106445085633E-5,
0.549405622560371));
#30624=CARTESIAN_POINT('Ctrl Pts',(-0.155272340811799,-0.0268780222436924,
0.55132440667186));
#30625=CARTESIAN_POINT('Ctrl Pts',(-0.135831396530156,-0.105747938365068,
0.556949404777722));
#30626=CARTESIAN_POINT('Ctrl Pts',(-0.0103102773360761,-0.183589824620028,
0.566280616877956));
#30627=CARTESIAN_POINT('Ctrl Pts',(0.14869956060099,-0.108166382022474,
0.577399258861071));
#30628=CARTESIAN_POINT('Ctrl Pts',(0.171494149863546,0.0663421591850832,
0.588517900844189));
#30629=CARTESIAN_POINT('Ctrl Pts',(0.0371926577693494,0.180078404398782,
0.599636542827304));
#30630=CARTESIAN_POINT('Ctrl Pts',(-0.118720103315053,0.132645343006727,
0.609932450066032));
#30631=CARTESIAN_POINT('Ctrl Pts',(-0.155195221197423,0.040094597399841,
0.616522143310387));
#30632=CARTESIAN_POINT('Ctrl Pts',(-0.155567057787938,-0.000141549514015748,
0.619405622560371));
#30633=CARTESIAN_POINT('Origin',(0.,0.,-0.129405622560369));
#30634=CARTESIAN_POINT('',(-0.155745492001379,-8.56371120316567E-5,0.46559437743963));
#30635=CARTESIAN_POINT('',(-0.155622585425313,0.000134239099646036,0.479405622560371));
#30636=CARTESIAN_POINT('',(-0.15555,-2.01987159101623E-14,-0.129405622560369));
#30637=CARTESIAN_POINT('Ctrl Pts',(-0.155745492001379,-8.56371120316864E-5,
0.465594377439631));
#30638=CARTESIAN_POINT('Ctrl Pts',(-0.15577850741697,-0.00506891626144068,
0.465952562306032));
#30639=CARTESIAN_POINT('Ctrl Pts',(-0.153301192978291,-0.0615473136307116,
0.470014468855281));
#30640=CARTESIAN_POINT('Ctrl Pts',(-0.0844041411881997,-0.163316067010957,
0.477780097087378));
#30641=CARTESIAN_POINT('Ctrl Pts',(0.0913973507436636,-0.159507746114991,
0.488891262135923));
#30642=CARTESIAN_POINT('Ctrl Pts',(0.183577980123458,-0.00976329900371924,
0.500002427184466));
#30643=CARTESIAN_POINT('Ctrl Pts',(0.10780025055099,0.148913742733129,0.51111359223301));
#30644=CARTESIAN_POINT('Ctrl Pts',(-0.0666056105926533,0.17134727727987,
0.522224757281553));
#30645=CARTESIAN_POINT('Ctrl Pts',(-0.149938299705611,0.0726891414718789,
0.530385019017093));
#30646=CARTESIAN_POINT('Ctrl Pts',(-0.155693038683329,0.0106378444150779,
0.534841559069786));
#30647=CARTESIAN_POINT('Ctrl Pts',(-0.155596383579478,0.000138071545366179,
0.53559437743963));
#30648=CARTESIAN_POINT('Ctrl Pts',(-0.155622585425313,0.000134239099646029,
0.479405622560371));
#30649=CARTESIAN_POINT('Ctrl Pts',(-0.155239700220769,-0.0418962472451577,
0.482420456038961));
#30650=CARTESIAN_POINT('Ctrl Pts',(-0.115964303797854,-0.136226320639006,
0.489141503511923));
#30651=CARTESIAN_POINT('Ctrl Pts',(0.0435376164803608,-0.17865050090601,
0.499568764979258));
#30652=CARTESIAN_POINT('Ctrl Pts',(0.173732980498774,-0.0602360109052031,
0.510687406962374));
#30653=CARTESIAN_POINT('Ctrl Pts',(0.144781397169404,0.113357278356683,
0.521806048945491));
#30654=CARTESIAN_POINT('Ctrl Pts',(-0.0167962271460079,0.183110382765203,
0.532924690928607));
#30655=CARTESIAN_POINT('Ctrl Pts',(-0.137758975876034,0.102035875886683,
0.542124548800234));
#30656=CARTESIAN_POINT('Ctrl Pts',(-0.155317332364345,0.0250672199885809,
0.547618192677488));
#30657=CARTESIAN_POINT('Ctrl Pts',(-0.15529563387483,1.51106445085633E-5,
0.549405622560371));
#30658=CARTESIAN_POINT('Origin',(0.,0.,-0.129405622560369));
#30659=CARTESIAN_POINT('',(-0.155339129538237,-8.2587420025254E-5,0.39559437743963));
#30660=CARTESIAN_POINT('',(-0.15573160577951,-9.4952305265919E-5,0.409405622560371));
#30661=CARTESIAN_POINT('',(-0.15555,-2.01987159101623E-14,-0.129405622560369));
#30662=CARTESIAN_POINT('Ctrl Pts',(-0.155339129538237,-8.25874200252562E-5,
0.39559437743963));
#30663=CARTESIAN_POINT('Ctrl Pts',(-0.155438295724494,-0.0206599346759669,
0.397063565542278));
#30664=CARTESIAN_POINT('Ctrl Pts',(-0.142062281789543,-0.0929876204718288,
0.402236475327773));
#30665=CARTESIAN_POINT('Ctrl Pts',(-0.0325213021862407,-0.180938005122649,
0.411113106796117));
#30666=CARTESIAN_POINT('Ctrl Pts',(0.134348911316817,-0.125485325124609,
0.42222427184466));
#30667=CARTESIAN_POINT('Ctrl Pts',(0.178301209192838,0.0447758371671112,
0.433335436893204));
#30668=CARTESIAN_POINT('Ctrl Pts',(0.0591229481908682,0.174070887258225,
0.444446601941748));
#30669=CARTESIAN_POINT('Ctrl Pts',(-0.10856218085317,0.145071736103991,
0.455199582123889));
#30670=CARTESIAN_POINT('Ctrl Pts',(-0.155437119708937,0.0464594445617744,
0.462248840623184));
#30671=CARTESIAN_POINT('Ctrl Pts',(-0.155745492001379,-8.56371120316864E-5,
0.465594377439631));
#30672=CARTESIAN_POINT('Ctrl Pts',(-0.15573160577951,-9.49523052659442E-5,
0.40940562256037));
#30673=CARTESIAN_POINT('Ctrl Pts',(-0.155772052747877,-0.00572626470532979,
0.40981029141169));
#30674=CARTESIAN_POINT('Ctrl Pts',(-0.152938259291224,-0.0628915705084586,
0.413921174257381));
#30675=CARTESIAN_POINT('Ctrl Pts',(-0.0822616502622442,-0.164452261823584,
0.421738271097444));
#30676=CARTESIAN_POINT('Ctrl Pts',(0.0936204134582059,-0.158261630557358,
0.43285691308056));
#30677=CARTESIAN_POINT('Ctrl Pts',(0.183742116834086,-0.00709647969689106,
0.443975555063676));
#30678=CARTESIAN_POINT('Ctrl Pts',(0.10554806974386,0.150569354438759,0.455094197046793));
#30679=CARTESIAN_POINT('Ctrl Pts',(-0.0693325883166112,0.170307127625589,
0.466212839029909));
#30680=CARTESIAN_POINT('Ctrl Pts',(-0.150503746143118,0.0709862178387775,
0.474316647534435));
#30681=CARTESIAN_POINT('Ctrl Pts',(-0.155710391061042,0.00977293375193425,
0.478714242044589));
#30682=CARTESIAN_POINT('Ctrl Pts',(-0.155622585425313,0.000134239099646029,
0.479405622560371));
#30683=CARTESIAN_POINT('Origin',(0.,0.,-0.129405622560369));
#30684=CARTESIAN_POINT('',(-0.155444674488022,0.000131742778884735,0.32559437743963));
#30685=CARTESIAN_POINT('',(-0.15533186684889,-7.70198572060954E-5,0.339405622560371));
#30686=CARTESIAN_POINT('',(-0.15555,-2.01987159101623E-14,-0.129405622560369));
#30687=CARTESIAN_POINT('Ctrl Pts',(-0.155444674488022,0.000131742778884739,
0.32559437743963));
#30688=CARTESIAN_POINT('Ctrl Pts',(-0.155154236665719,-0.0359445316439912,
0.328174568778523));
#30689=CARTESIAN_POINT('Ctrl Pts',(-0.124691611905359,-0.124248704432008,
0.334458481800264));
#30690=CARTESIAN_POINT('Ctrl Pts',(0.0222506403513669,-0.18248590575151,
0.344446116504855));
#30691=CARTESIAN_POINT('Ctrl Pts',(0.165365282072159,-0.0803151310699741,
0.355557281553397));
#30692=CARTESIAN_POINT('Ctrl Pts',(0.157184646516792,0.0953372104320743,
0.366668446601942));
#30693=CARTESIAN_POINT('Ctrl Pts',(0.00519332482321354,0.183764050268212,
0.377779611650485));
#30694=CARTESIAN_POINT('Ctrl Pts',(-0.130823935507303,0.114600960175539,
0.387421588596382));
#30695=CARTESIAN_POINT('Ctrl Pts',(-0.155188304621527,0.0312141358191517,
0.39335984385943));
#30696=CARTESIAN_POINT('Ctrl Pts',(-0.155339129538237,-8.25874200252562E-5,
0.39559437743963));
#30697=CARTESIAN_POINT('Ctrl Pts',(-0.15533186684889,-7.70198572060919E-5,
0.339405622560371));
#30698=CARTESIAN_POINT('Ctrl Pts',(-0.155425971941861,-0.0210984061911746,
0.34090634077879));
#30699=CARTESIAN_POINT('Ctrl Pts',(-0.141654850766895,-0.0939166341982764,
0.346113272991582));
#30700=CARTESIAN_POINT('Ctrl Pts',(-0.0308692884081366,-0.181269447386996,
0.355026419198746));
#30701=CARTESIAN_POINT('Ctrl Pts',(0.135606994996762,-0.124186426112907,
0.366145061181863));
#30702=CARTESIAN_POINT('Ctrl Pts',(0.177861387826841,0.0466567491694538,
0.377263703164979));
#30703=CARTESIAN_POINT('Ctrl Pts',(0.0571870330903418,0.174760318061885,
0.388382345148095));
#30704=CARTESIAN_POINT('Ctrl Pts',(-0.109574509035902,0.143939945308724,
0.399096318279893));
#30705=CARTESIAN_POINT('Ctrl Pts',(-0.155401613758806,0.0458488658137791,
0.406104077417318));
#30706=CARTESIAN_POINT('Ctrl Pts',(-0.15573160577951,-9.49523052659442E-5,
0.40940562256037));
#30707=CARTESIAN_POINT('Origin',(0.,0.,-0.129405622560369));
#30708=CARTESIAN_POINT('',(-0.155804712705668,3.25009013604671E-6,0.25559437743963));
#30709=CARTESIAN_POINT('',(-0.155449947323643,0.000133480041304715,0.269405622560371));
#30710=CARTESIAN_POINT('',(-0.15555,-2.01987159101623E-14,-0.129405622560369));
#30711=CARTESIAN_POINT('Ctrl Pts',(-0.155804712705668,3.25009013604029E-6,
0.25559437743963));
#30712=CARTESIAN_POINT('Ctrl Pts',(-0.155788927539753,-0.0512989453804214,
0.259285572014769));
#30713=CARTESIAN_POINT('Ctrl Pts',(-0.10006227616332,-0.154106832868198,
0.266680488272757));
#30714=CARTESIAN_POINT('Ctrl Pts',(0.0750458968510211,-0.167822257683237,
0.277779126213592));
#30715=CARTESIAN_POINT('Ctrl Pts',(0.181691053470019,-0.0280099604209337,
0.288890291262136));
#30716=CARTESIAN_POINT('Ctrl Pts',(0.122104229764526,0.137429086670804,
0.30000145631068));
#30717=CARTESIAN_POINT('Ctrl Pts',(-0.0491976593161155,0.177132117679823,
0.311112621359223));
#30718=CARTESIAN_POINT('Ctrl Pts',(-0.146161229246342,0.0831876851886141,
0.319643595068874));
#30719=CARTESIAN_POINT('Ctrl Pts',(-0.155571144064704,0.0158409610837222,
0.324470847095676));
#30720=CARTESIAN_POINT('Ctrl Pts',(-0.155444674488022,0.000131742778884739,
0.32559437743963));
#30721=CARTESIAN_POINT('Ctrl Pts',(-0.155449947323643,0.000133480041304701,
0.269405622560371));
#30722=CARTESIAN_POINT('Ctrl Pts',(-0.155153406972295,-0.0361714100102126,
0.272002390145891));
#30723=CARTESIAN_POINT('Ctrl Pts',(-0.12437032104418,-0.124745277135715,
0.278305371725784));
#30724=CARTESIAN_POINT('Ctrl Pts',(0.0231926238140432,-0.182410602009977,
0.288314567300049));
#30725=CARTESIAN_POINT('Ctrl Pts',(0.165866396469461,-0.0793716828903688,
0.299433209283165));
#30726=CARTESIAN_POINT('Ctrl Pts',(0.156599354026699,0.096375141196464,
0.310551851266282));
#30727=CARTESIAN_POINT('Ctrl Pts',(0.00388050940998321,0.183838154825996,
0.321670493249398));
#30728=CARTESIAN_POINT('Ctrl Pts',(-0.131300314367493,0.113822266482633,
0.331288417014094));
#30729=CARTESIAN_POINT('Ctrl Pts',(-0.155193567478298,0.0308165737536199,
0.337200126784418));
#30730=CARTESIAN_POINT('Ctrl Pts',(-0.15533186684889,-7.70198572060919E-5,
0.339405622560371));
#30731=CARTESIAN_POINT('Origin',(0.,0.,-0.129405622560369));
#30732=CARTESIAN_POINT('',(-0.155454118234884,-0.000133834695600709,0.18559437743963));
#30733=CARTESIAN_POINT('',(-0.155805467550008,3.4854191793785E-6,0.19940562256037));
#30734=CARTESIAN_POINT('',(-0.15555,-2.01987159101623E-14,-0.129405622560369));
#30735=CARTESIAN_POINT('Ctrl Pts',(-0.155454118234884,-0.000133834695600729,
0.18559437743963));
#30736=CARTESIAN_POINT('Ctrl Pts',(-0.155580288786201,-0.0154903851691022,
0.186692853568168));
#30737=CARTESIAN_POINT('Ctrl Pts',(-0.146436232298065,-0.0824775316270878,
0.191495051379553));
#30738=CARTESIAN_POINT('Ctrl Pts',(-0.0503915664640746,-0.176796168665343,
0.200000970873786));
#30739=CARTESIAN_POINT('Ctrl Pts',(0.121174280763407,-0.138249741391359,
0.21111213592233));
#30740=CARTESIAN_POINT('Ctrl Pts',(0.181875888824183,0.0267835396201195,
0.222223300970874));
#30741=CARTESIAN_POINT('Ctrl Pts',(0.0761764071097843,0.167312138149853,
0.233334466019417));
#30742=CARTESIAN_POINT('Ctrl Pts',(-0.0992180579104728,0.154764252547341,
0.244445631067961));
#30743=CARTESIAN_POINT('Ctrl Pts',(-0.155725669913861,0.0518277207581445,
0.251865601541365));
#30744=CARTESIAN_POINT('Ctrl Pts',(-0.155804766277071,0.00017735852989955,
0.255581850331921));
#30745=CARTESIAN_POINT('Ctrl Pts',(-0.155804712705668,3.25009013604029E-6,
0.25559437743963));
#30746=CARTESIAN_POINT('Ctrl Pts',(-0.155805467550008,3.48541917938314E-6,
0.19940562256037));
#30747=CARTESIAN_POINT('Ctrl Pts',(-0.155788564535512,-0.0513206116891616,
0.203098439512992));
#30748=CARTESIAN_POINT('Ctrl Pts',(-0.100003893378143,-0.154186484140614,
0.210497470459985));
#30749=CARTESIAN_POINT('Ctrl Pts',(0.0752488571272716,-0.167777039880966,
0.221602715401351));
#30750=CARTESIAN_POINT('Ctrl Pts',(0.181781810074028,-0.0276929424335053,
0.232721357384467));
#30751=CARTESIAN_POINT('Ctrl Pts',(0.121794738393109,0.137759091140133,
0.243839999367584));
#30752=CARTESIAN_POINT('Ctrl Pts',(-0.0497615974795104,0.177017821004958,
0.2549586413507));
#30753=CARTESIAN_POINT('Ctrl Pts',(-0.146313162187878,0.0828233020270418,
0.263480515748296));
#30754=CARTESIAN_POINT('Ctrl Pts',(-0.155576641614544,0.0156444291597347,
0.268296176151519));
#30755=CARTESIAN_POINT('Ctrl Pts',(-0.155449947323643,0.000133480041304701,
0.269405622560371));
#30756=CARTESIAN_POINT('Origin',(0.,0.,-0.129405622560369));
#30757=CARTESIAN_POINT('',(-0.155333634177863,7.79921548230329E-5,0.11559437743963));
#30758=CARTESIAN_POINT('',(-0.155460191805193,-0.000135568056800359,0.12940562256037));
#30759=CARTESIAN_POINT('',(-0.15555,-2.01987159101623E-14,-0.129405622560369));
#30760=CARTESIAN_POINT('Ctrl Pts',(-0.155333634177863,7.79921548230561E-5,
0.11559437743963));
#30761=CARTESIAN_POINT('Ctrl Pts',(-0.155193438638927,-0.0308706275100063,
0.117803856804414));
#30762=CARTESIAN_POINT('Ctrl Pts',(-0.131241956589738,-0.11389814578602,
0.123717057852045));
#30763=CARTESIAN_POINT('Ctrl Pts',(0.00395347168138628,-0.183794704008407,
0.133333980582524));
#30764=CARTESIAN_POINT('Ctrl Pts',(0.156537855283131,-0.0963955976349113,
0.144445145631068));
#30765=CARTESIAN_POINT('Ctrl Pts',(0.165903376979378,0.0791977165381959,
0.155556310679611));
#30766=CARTESIAN_POINT('Ctrl Pts',(0.0234812759114929,0.182331608910266,
0.166667475728155));
#30767=CARTESIAN_POINT('Ctrl Pts',(-0.124220109658982,0.124943524423025,
0.176680164648161));
#30768=CARTESIAN_POINT('Ctrl Pts',(-0.155154880719052,0.0362871523529771,
0.18298913188532));
#30769=CARTESIAN_POINT('Ctrl Pts',(-0.155454118234884,-0.000133834695600729,
0.18559437743963));
#30770=CARTESIAN_POINT('Ctrl Pts',(-0.155460191805193,-0.000135568056800364,
0.12940562256037));
#30771=CARTESIAN_POINT('Ctrl Pts',(-0.15558637635503,-0.0152693971168416,
0.130488274885721));
#30772=CARTESIAN_POINT('Ctrl Pts',(-0.146605510259419,-0.0820638709603335,
0.135277141205443));
#30773=CARTESIAN_POINT('Ctrl Pts',(-0.0510374815939226,-0.176654153931159,
0.143772221519537));
#30774=CARTESIAN_POINT('Ctrl Pts',(0.120797626960931,-0.138634273102519,
0.154890863502654));
#30775=CARTESIAN_POINT('Ctrl Pts',(0.181976886629041,0.0263806680570579,
0.16600950548577));
#30776=CARTESIAN_POINT('Ctrl Pts',(0.0764574137846417,0.167229745635935,
0.177128147468886));
#30777=CARTESIAN_POINT('Ctrl Pts',(-0.0991003621173195,0.154889135395602,
0.188246789452002));
#30778=CARTESIAN_POINT('Ctrl Pts',(-0.15572087700955,0.0518861158146895,
0.195672614482497));
#30779=CARTESIAN_POINT('Ctrl Pts',(-0.155805528871865,0.000189682319971778,
0.19939222551862));
#30780=CARTESIAN_POINT('Ctrl Pts',(-0.155805467550008,3.48541917938314E-6,
0.19940562256037));
#30781=CARTESIAN_POINT('Origin',(0.,0.,-0.129405622560369));
#30782=CARTESIAN_POINT('',(-0.155735926886437,0.000101346774827271,0.0455943774396301));
#30783=CARTESIAN_POINT('',(-0.155326046963413,7.29270061605516E-5,0.0594056225603705));
#30784=CARTESIAN_POINT('',(-0.15555,-2.01987159101623E-14,-0.129405622560369));
#30785=CARTESIAN_POINT('Ctrl Pts',(-0.155735926886437,0.000101346774827265,
0.0455943774396301));
#30786=CARTESIAN_POINT('Ctrl Pts',(-0.15541538777776,-0.0460983628495037,
0.0489148600406595));
#30787=CARTESIAN_POINT('Ctrl Pts',(-0.109151218308356,-0.144423481489054,
0.0559390643245367));
#30788=CARTESIAN_POINT('Ctrl Pts',(0.0579488995883613,-0.174456230311225,
0.0666669902912619));
#30789=CARTESIAN_POINT('Ctrl Pts',(0.177994191588978,-0.0459827600750814,
0.0777781553398056));
#30790=CARTESIAN_POINT('Ctrl Pts',(0.135192905881154,0.124578720765632,
0.0888893203883492));
#30791=CARTESIAN_POINT('Ctrl Pts',(-0.0313001003158473,0.181151906168851,
0.100000485436893));
#30792=CARTESIAN_POINT('Ctrl Pts',(-0.141742497137191,0.093698092273704,
0.108902171120653));
#30793=CARTESIAN_POINT('Ctrl Pts',(-0.155428446607623,0.0210081433596544,
0.114100135121566));
#30794=CARTESIAN_POINT('Ctrl Pts',(-0.155333634177863,7.79921548230561E-5,
0.11559437743963));
#30795=CARTESIAN_POINT('Ctrl Pts',(-0.155326046963413,7.29270061605551E-5,
0.0594056225603705));
#30796=CARTESIAN_POINT('Ctrl Pts',(-0.155199262831984,-0.0304485333833814,
0.0615843242528215));
#30797=CARTESIAN_POINT('Ctrl Pts',(-0.131743653601245,-0.113071739766558,
0.0674692399396446));
#30798=CARTESIAN_POINT('Ctrl Pts',(0.00255447675030308,-0.183860034663711,
0.0770603696208398));
#30799=CARTESIAN_POINT('Ctrl Pts',(0.155899683301632,-0.0975032021788082,
0.0881790116039561));
#30800=CARTESIAN_POINT('Ctrl Pts',(0.166434877052597,0.0781732535368643,
0.0992976535870723));
#30801=CARTESIAN_POINT('Ctrl Pts',(0.0245080507541896,0.182238325373942,
0.110416295570189));
#30802=CARTESIAN_POINT('Ctrl Pts',(-0.123863138927055,0.125487925833816,
0.120452285227955));
#30803=CARTESIAN_POINT('Ctrl Pts',(-0.155154412248428,0.0365378245899198,
0.126782060891349));
#30804=CARTESIAN_POINT('Ctrl Pts',(-0.155460191805193,-0.000135568056800364,
0.12940562256037));
#30805=CARTESIAN_POINT('Origin',(0.,0.,1.15));
#30806=CARTESIAN_POINT('',(-0.177892626630995,-0.00012009523392913,1.12223275485995));
#30807=CARTESIAN_POINT('Ctrl Pts',(0.155548765964692,0.000619602180104872,
1.14445));
#30808=CARTESIAN_POINT('Ctrl Pts',(0.156083861551471,-0.0102125174737046,
1.14395805623115));
#30809=CARTESIAN_POINT('Ctrl Pts',(0.15539846640382,-0.0210404421466269,
1.14347026853365));
#30810=CARTESIAN_POINT('Ctrl Pts',(0.153608590638952,-0.0317127652002419,
1.14298392615444));
#30811=CARTESIAN_POINT('Ctrl Pts',(0.152914716720618,-0.0358500616318106,
1.14279538776594));
#30812=CARTESIAN_POINT('Ctrl Pts',(0.152054287987853,-0.0399640361908485,
1.14260706658696));
#30813=CARTESIAN_POINT('Ctrl Pts',(0.151032028551573,-0.0440458121014301,
1.1424188046881));
#30814=CARTESIAN_POINT('Ctrl Pts',(0.150071136707034,-0.0478825535826186,
1.14224184440107));
#30815=CARTESIAN_POINT('Ctrl Pts',(0.148969254907822,-0.0516824965112672,
1.14206531990211));
#30816=CARTESIAN_POINT('Ctrl Pts',(0.147732675525468,-0.0554351396328931,
1.14188926057926));
#30817=CARTESIAN_POINT('Ctrl Pts',(0.144705099540774,-0.0646229138722882,
1.14145820618411));
#30818=CARTESIAN_POINT('Ctrl Pts',(0.14087037084284,-0.0735342808861364,
1.14102963880076));
#30819=CARTESIAN_POINT('Ctrl Pts',(0.136287966367236,-0.0820616333277537,
1.14060170770949));
#30820=CARTESIAN_POINT('Ctrl Pts',(0.134099734044687,-0.0861336938230361,
1.1403973580824));
#30821=CARTESIAN_POINT('Ctrl Pts',(0.131738457084688,-0.090120565054425,
1.14019301071694));
#30822=CARTESIAN_POINT('Ctrl Pts',(0.129223539536337,-0.0939888668888786,
1.1399895855729));
#30823=CARTESIAN_POINT('Ctrl Pts',(0.123841150615535,-0.102267748615928,
1.1395542181223));
#30824=CARTESIAN_POINT('Ctrl Pts',(0.117747056171278,-0.110025200831312,
1.1391220629978));
#30825=CARTESIAN_POINT('Ctrl Pts',(0.11100116606729,-0.117148456023219,
1.13869123413476));
#30826=CARTESIAN_POINT('Ctrl Pts',(0.106906026602935,-0.121472677586479,
1.13842969647966));
#30827=CARTESIAN_POINT('Ctrl Pts',(0.102570142764087,-0.125562999006382,
1.13816864757596));
#30828=CARTESIAN_POINT('Ctrl Pts',(0.0980025572591369,-0.129390839920029,
1.13790766548932));
#30829=CARTESIAN_POINT('Ctrl Pts',(0.0956731876101781,-0.131342955854285,
1.13777457027942));
#30830=CARTESIAN_POINT('Ctrl Pts',(0.0932817165779503,-0.133228060285772,
1.13764139558094));
#30831=CARTESIAN_POINT('Ctrl Pts',(0.0908350990518728,-0.135037587415829,
1.1375084117344));
#30832=CARTESIAN_POINT('Ctrl Pts',(0.0901763381324703,-0.135524809363345,
1.13747260533636));
#30833=CARTESIAN_POINT('Ctrl Pts',(0.0895137718121014,-0.136006421121091,
1.1374368229172));
#30834=CARTESIAN_POINT('Ctrl Pts',(0.0888474357058895,-0.136482361432558,
1.13740106343829));
#30835=CARTESIAN_POINT('Ctrl Pts',(0.0798411198483208,-0.142915254284167,
1.1369177320399));
#30836=CARTESIAN_POINT('Ctrl Pts',(0.0701492813036541,-0.148315340119806,
1.1364385915245));
#30837=CARTESIAN_POINT('Ctrl Pts',(0.059971176200061,-0.152699426079087,
1.13596107719954));
#30838=CARTESIAN_POINT('Ctrl Pts',(0.0530631196487977,-0.155674981295315,
1.13563697994103));
#30839=CARTESIAN_POINT('Ctrl Pts',(0.0459300802687867,-0.158181722966519,
1.13531363179894));
#30840=CARTESIAN_POINT('Ctrl Pts',(0.0386275637501033,-0.16021396300419,
1.13499023090658));
#30841=CARTESIAN_POINT('Ctrl Pts',(0.0351988940876516,-0.161168138149998,
1.13483838806916));
#30842=CARTESIAN_POINT('Ctrl Pts',(0.0317324236549294,-0.162017357570902,
1.13468652012024));
#30843=CARTESIAN_POINT('Ctrl Pts',(0.028249074324747,-0.162757963065587,
1.13453519958799));
#30844=CARTESIAN_POINT('Ctrl Pts',(0.0167982212800381,-0.165192563755867,
1.13403776191718));
#30845=CARTESIAN_POINT('Ctrl Pts',(0.00512774808450533,-0.166468890755321,
1.13354451715097));
#30846=CARTESIAN_POINT('Ctrl Pts',(-0.00655533748915361,-0.166579173106486,
1.13305265956701));
#30847=CARTESIAN_POINT('Ctrl Pts',(-0.0141044995850598,-0.166650433334789,
1.1327348400487));
#30848=CARTESIAN_POINT('Ctrl Pts',(-0.0216594951399176,-0.166233867742642,
1.13241759971353));
#30849=CARTESIAN_POINT('Ctrl Pts',(-0.0291655735035569,-0.165315833865676,
1.13210018160962));
#30850=CARTESIAN_POINT('Ctrl Pts',(-0.0327092118793667,-0.164882427775424,
1.13195032772857));
#30851=CARTESIAN_POINT('Ctrl Pts',(-0.0362323925945039,-0.164338226995567,
1.13180083633464));
#30852=CARTESIAN_POINT('Ctrl Pts',(-0.0397271405986897,-0.163683459359474,
1.13165172827032));
#30853=CARTESIAN_POINT('Ctrl Pts',(-0.0499359232133337,-0.16177076624055,
1.13121615700369));
#30854=CARTESIAN_POINT('Ctrl Pts',(-0.0599087164806791,-0.158916175424461,
1.13078358684414));
#30855=CARTESIAN_POINT('Ctrl Pts',(-0.0695044280650932,-0.155097228857054,
1.13035212687658));
#30856=CARTESIAN_POINT('Ctrl Pts',(-0.0757996376989387,-0.152591831627178,
1.1300690701256));
#30857=CARTESIAN_POINT('Ctrl Pts',(-0.0819325841193579,-0.149670688079838,
1.12978649119439));
#30858=CARTESIAN_POINT('Ctrl Pts',(-0.0878818038415969,-0.146365274834167,
1.12950385616925));
#30859=CARTESIAN_POINT('Ctrl Pts',(-0.0910874459297812,-0.144584205666465,
1.12935156279727));
#30860=CARTESIAN_POINT('Ctrl Pts',(-0.09424019426452,-0.142690781721644,
1.129199221353));
#30861=CARTESIAN_POINT('Ctrl Pts',(-0.0973230172632952,-0.140698989172901,
1.12904742410559));
#30862=CARTESIAN_POINT('Ctrl Pts',(-0.107217543799977,-0.134306197813512,
1.12856022069066));
#30863=CARTESIAN_POINT('Ctrl Pts',(-0.116428399613608,-0.126885604548101,
1.12807698662012));
#30864=CARTESIAN_POINT('Ctrl Pts',(-0.124852487683086,-0.118613771136687,
1.12759508954235));
#30865=CARTESIAN_POINT('Ctrl Pts',(-0.129034307879819,-0.114507532011624,
1.12735586994778));
#30866=CARTESIAN_POINT('Ctrl Pts',(-0.133021908645802,-0.110190752518543,
1.12711697982177));
#30867=CARTESIAN_POINT('Ctrl Pts',(-0.136799920681752,-0.105681293454548,
1.12687809715289));
#30868=CARTESIAN_POINT('Ctrl Pts',(-0.139913092404994,-0.101965391993263,
1.12668125215535));
#30869=CARTESIAN_POINT('Ctrl Pts',(-0.142886395744951,-0.0981144149624532,
1.12648421657965));
#30870=CARTESIAN_POINT('Ctrl Pts',(-0.145693560119959,-0.0941626751454851,
1.12628802354802));
#30871=CARTESIAN_POINT('Ctrl Pts',(-0.152880478586678,-0.0840454080131806,
1.12578572901386));
#30872=CARTESIAN_POINT('Ctrl Pts',(-0.15900482121196,-0.0732463252276768,
1.12528759909576));
#30873=CARTESIAN_POINT('Ctrl Pts',(-0.163934147646496,-0.0619414999212126,
1.12479074962784));
#30874=CARTESIAN_POINT('Ctrl Pts',(-0.166135734382546,-0.0568924219632783,
1.1245688415816));
#30875=CARTESIAN_POINT('Ctrl Pts',(-0.168098373685913,-0.0517419572379162,
1.12434718895784));
#30876=CARTESIAN_POINT('Ctrl Pts',(-0.169806974463718,-0.0465039785200352,
1.12412553479695));
#30877=CARTESIAN_POINT('Ctrl Pts',(-0.171302024805205,-0.0419206715400791,
1.12393158420695));
#30878=CARTESIAN_POINT('Ctrl Pts',(-0.172603159720904,-0.037265702966286,
1.12373744627196));
#30879=CARTESIAN_POINT('Ctrl Pts',(-0.173693332107248,-0.0325769359939504,
1.12354412603317));
#30880=CARTESIAN_POINT('Ctrl Pts',(-0.174146803491923,-0.0306265823819912,
1.12346371196521));
#30881=CARTESIAN_POINT('Ctrl Pts',(-0.174564098410947,-0.0286695573112724,
1.12338340400172));
#30882=CARTESIAN_POINT('Ctrl Pts',(-0.174944665354966,-0.0267065873422436,
1.12330319031487));
#30883=CARTESIAN_POINT('Ctrl Pts',(-0.176644787249262,-0.0179373332737037,
1.1229448485109));
#30884=CARTESIAN_POINT('Ctrl Pts',(-0.177613299278372,-0.00904985393428815,
1.12258838819752));
#30885=CARTESIAN_POINT('Ctrl Pts',(-0.177892626630995,-0.00012009523392913,
1.12223275485995));
#30886=CARTESIAN_POINT('',(0.188128289424299,-0.051655738433239,1.1046));
#30887=CARTESIAN_POINT('Ctrl Pts',(0.188079991776263,-0.0516378774142054,
1.1046));
#30888=CARTESIAN_POINT('Ctrl Pts',(0.189767230432996,-0.0390669740826218,
1.10628778184834));
#30889=CARTESIAN_POINT('Ctrl Pts',(0.190280594088308,-0.0264116239428061,
1.10798825493552));
#30890=CARTESIAN_POINT('Ctrl Pts',(0.189578785198131,-0.013858618669063,
1.10971174069725));
#30891=CARTESIAN_POINT('Ctrl Pts',(0.189002564675101,-0.00355196771938053,
1.11112680950153));
#30892=CARTESIAN_POINT('Ctrl Pts',(0.187606197243972,0.00668612269204304,
1.11255739169934));
#30893=CARTESIAN_POINT('Ctrl Pts',(0.185342457317502,0.0167394104911895,
1.1140092000994));
#30894=CARTESIAN_POINT('Ctrl Pts',(0.184551132811226,0.0202536891903846,
1.1145167016688));
#30895=CARTESIAN_POINT('Ctrl Pts',(0.183655673454389,0.0237360512197014,
1.1150254747949));
#30896=CARTESIAN_POINT('Ctrl Pts',(0.18265534113529,0.0271808706561584,
1.11553563926267));
#30897=CARTESIAN_POINT('Ctrl Pts',(0.18094879298457,0.0330576679230306,
1.11640597026411));
#30898=CARTESIAN_POINT('Ctrl Pts',(0.178936945382248,0.038826456249319,
1.11728051290445));
#30899=CARTESIAN_POINT('Ctrl Pts',(0.176612263817241,0.0444636415640588,
1.1181607012295));
#30900=CARTESIAN_POINT('Ctrl Pts',(0.172529449099474,0.0543641731105064,
1.11970656708142));
#30901=CARTESIAN_POINT('Ctrl Pts',(0.167482382247398,0.0638604192469179,
1.12126984735358));
#30902=CARTESIAN_POINT('Ctrl Pts',(0.161567727140847,0.0728508334626257,
1.12285831080443));
#30903=CARTESIAN_POINT('Ctrl Pts',(0.159791310571961,0.0755510282307451,
1.12333539234888));
#30904=CARTESIAN_POINT('Ctrl Pts',(0.157935831204718,0.07820633305328,1.12381491808146));
#30905=CARTESIAN_POINT('Ctrl Pts',(0.156005857937656,0.080810555607592,
1.12429655968642));
#30906=CARTESIAN_POINT('Ctrl Pts',(0.149084780910453,0.0901495579668382,
1.12602377461955));
#30907=CARTESIAN_POINT('Ctrl Pts',(0.141258220296783,0.0987686403112959,
1.12776582990404));
#30908=CARTESIAN_POINT('Ctrl Pts',(0.132662596065602,0.106547632773669,
1.12953438681126));
#30909=CARTESIAN_POINT('Ctrl Pts',(0.125865807878512,0.11269868854969,1.13093283169111));
#30910=CARTESIAN_POINT('Ctrl Pts',(0.11858709408701,0.11832389399092,1.13234784666969));
#30911=CARTESIAN_POINT('Ctrl Pts',(0.110887722236713,0.123341541992538,
1.13378519708595));
#30912=CARTESIAN_POINT('Ctrl Pts',(0.108018415924993,0.125211456754541,
1.13432085099405));
#30913=CARTESIAN_POINT('Ctrl Pts',(0.105090557092059,0.126996521585399,
1.13485961189033));
#30914=CARTESIAN_POINT('Ctrl Pts',(0.102119703918859,0.128685646974318,
1.13539959124502));
#30915=CARTESIAN_POINT('Ctrl Pts',(0.0927768272952827,0.133997686711853,
1.13709774332326));
#30916=CARTESIAN_POINT('Ctrl Pts',(0.082979544177925,0.138384526176108,
1.13881348137989));
#30917=CARTESIAN_POINT('Ctrl Pts',(0.0728343136972591,0.141721417442936,
1.14055808556308));
#30918=CARTESIAN_POINT('Ctrl Pts',(0.0653892612002304,0.144170186912073,
1.14183835906254));
#30919=CARTESIAN_POINT('Ctrl Pts',(0.0577564921504827,0.146052612758731,
1.14313417790127));
#30920=CARTESIAN_POINT('Ctrl Pts',(0.0499806597877626,0.147301514408983,
1.14445));
#30921=CARTESIAN_POINT('',(0.156060797133591,0.117265290216009,1.1046));
#30922=CARTESIAN_POINT('Origin',(0.,0.,1.1046));
#30923=CARTESIAN_POINT('Ctrl Pts',(-0.177892626630995,-0.00012009523392913,
1.12223275485995));
#30924=CARTESIAN_POINT('Ctrl Pts',(-0.178130827469488,0.00749489839273535,
1.12192948288029));
#30925=CARTESIAN_POINT('Ctrl Pts',(-0.177867516731744,0.0151409018269471,
1.12162681218094));
#30926=CARTESIAN_POINT('Ctrl Pts',(-0.177119648653777,0.022772046405986,
1.12132408898598));
#30927=CARTESIAN_POINT('Ctrl Pts',(-0.176683933562239,0.0272180241883703,
1.12114771955869));
#30928=CARTESIAN_POINT('Ctrl Pts',(-0.176082727329522,0.0316616978614784,
1.1209712215835));
#30929=CARTESIAN_POINT('Ctrl Pts',(-0.175323410854016,0.0360699258071878,
1.12079542245302));
#30930=CARTESIAN_POINT('Ctrl Pts',(-0.173218074679692,0.0482924997380182,
1.12030798897732));
#30931=CARTESIAN_POINT('Ctrl Pts',(-0.169899117173377,0.060280772698104,
1.11982442300823));
#30932=CARTESIAN_POINT('Ctrl Pts',(-0.165450405286176,0.0718434015054524,
1.11934209182814));
#30933=CARTESIAN_POINT('Ctrl Pts',(-0.163468469691568,0.0769946421750163,
1.11912720955245));
#30934=CARTESIAN_POINT('Ctrl Pts',(-0.161261595477516,0.0820613755489734,
1.11891257235417));
#30935=CARTESIAN_POINT('Ctrl Pts',(-0.158833971908418,0.0870258740589896,
1.11869794744021));
#30936=CARTESIAN_POINT('Ctrl Pts',(-0.157259648823123,0.0902453701582717,
1.11855876237008));
#30937=CARTESIAN_POINT('Ctrl Pts',(-0.155591255289476,0.0934239508703652,
1.11841948892714));
#30938=CARTESIAN_POINT('Ctrl Pts',(-0.153833447558489,0.0965496328988143,
1.11828037128997));
#30939=CARTESIAN_POINT('Ctrl Pts',(-0.14771977559034,0.10742078465325,1.11779651882779));
#30940=CARTESIAN_POINT('Ctrl Pts',(-0.140558745189236,0.117602653899592,
1.11731683957354));
#30941=CARTESIAN_POINT('Ctrl Pts',(-0.132418289468816,0.126903043139938,
1.11683877992991));
#30942=CARTESIAN_POINT('Ctrl Pts',(-0.12909688936255,0.130697709540948,
1.11664372606491));
#30943=CARTESIAN_POINT('Ctrl Pts',(-0.125611892721837,0.134345412680643,
1.11644894182206));
#30944=CARTESIAN_POINT('Ctrl Pts',(-0.121965775424868,0.137831740927343,
1.11625425375315));
#30945=CARTESIAN_POINT('Ctrl Pts',(-0.117995359394073,0.141628155697328,
1.11604224942997));
#30946=CARTESIAN_POINT('Ctrl Pts',(-0.113833879872902,0.145233242900832,
1.11583035914965));
#30947=CARTESIAN_POINT('Ctrl Pts',(-0.109497995542763,0.148643456469952,
1.11561835894421));
#30948=CARTESIAN_POINT('Ctrl Pts',(-0.106528819965926,0.150978740824945,
1.11547318306212));
#30949=CARTESIAN_POINT('Ctrl Pts',(-0.103484861618328,0.153216986140016,
1.11532830099587));
#30950=CARTESIAN_POINT('Ctrl Pts',(-0.100375391374892,0.155356036404444,
1.11518378070706));
#30951=CARTESIAN_POINT('Ctrl Pts',(-0.0901590665073864,0.162383996377836,
1.11470895184398));
#30952=CARTESIAN_POINT('Ctrl Pts',(-0.0792284020877703,0.168351899996775,
1.11423755053895));
#30953=CARTESIAN_POINT('Ctrl Pts',(-0.0677866372531476,0.173236468334987,
1.11376713654095));
#30954=CARTESIAN_POINT('Ctrl Pts',(-0.0629527485252524,0.175300088779209,
1.11356839718953));
#30955=CARTESIAN_POINT('Ctrl Pts',(-0.0580272205709242,0.1771698553942,
1.11336983405985));
#30956=CARTESIAN_POINT('Ctrl Pts',(-0.053024031320765,0.178841703955505,
1.11317126314023));
#30957=CARTESIAN_POINT('Ctrl Pts',(-0.0477983789695303,0.180587890023723,
1.11296386291187));
#30958=CARTESIAN_POINT('Ctrl Pts',(-0.0424815416125505,0.182119285098682,
1.11275621043829));
#30959=CARTESIAN_POINT('Ctrl Pts',(-0.0371242414709178,0.183422331662166,
1.11254943891139));
#30960=CARTESIAN_POINT('Ctrl Pts',(-0.024630778610864,0.18646109436267,
1.11206723848886));
#30961=CARTESIAN_POINT('Ctrl Pts',(-0.0118919597510465,0.188273325293319,
1.11158873863955));
#30962=CARTESIAN_POINT('Ctrl Pts',(0.000886208579909016,0.188815541438236,
1.11111139386139));
#30963=CARTESIAN_POINT('Ctrl Pts',(0.00944159770367764,0.189178572350712,
1.1107917963872));
#30964=CARTESIAN_POINT('Ctrl Pts',(0.018015230692156,0.18897135417352,1.11047271669991));
#30965=CARTESIAN_POINT('Ctrl Pts',(0.0265466554166013,0.188167601942836,
1.11015339081081));
#30966=CARTESIAN_POINT('Ctrl Pts',(0.0302389326862781,0.187819749598396,
1.11001519118297));
#30967=CARTESIAN_POINT('Ctrl Pts',(0.0339178177085591,0.187360375525866,
1.1098771490423));
#30968=CARTESIAN_POINT('Ctrl Pts',(0.0375710017615334,0.186789297951633,
1.1097394835104));
#30969=CARTESIAN_POINT('Ctrl Pts',(0.0423078408099154,0.186048819915471,
1.10956098183688));
#30970=CARTESIAN_POINT('Ctrl Pts',(0.0470053189021468,0.185120233668386,
1.10938296950455));
#30971=CARTESIAN_POINT('Ctrl Pts',(0.0516529562716852,0.184000805096474,
1.10920531719144));
#30972=CARTESIAN_POINT('Ctrl Pts',(0.0618028867738203,0.181556095816553,
1.10881734401536));
#30973=CARTESIAN_POINT('Ctrl Pts',(0.0717155486830652,0.178202889727245,
1.10843108790673));
#30974=CARTESIAN_POINT('Ctrl Pts',(0.0813183120370126,0.174031280266035,
1.10804520187417));
#30975=CARTESIAN_POINT('Ctrl Pts',(0.0859478038432918,0.172020147521446,
1.10785916623421));
#30976=CARTESIAN_POINT('Ctrl Pts',(0.0905051909798001,0.169818426512715,
1.10767321660747));
#30977=CARTESIAN_POINT('Ctrl Pts',(0.0949816305437677,0.167434340091183,
1.10748720206377));
#30978=CARTESIAN_POINT('Ctrl Pts',(0.0983118022353031,0.165660739219842,
1.10734881968224));
#30979=CARTESIAN_POINT('Ctrl Pts',(0.101597049834463,0.16378593049508,1.10721040073536));
#30980=CARTESIAN_POINT('Ctrl Pts',(0.104821419449008,0.161821258958598,
1.10707241581092));
#30981=CARTESIAN_POINT('Ctrl Pts',(0.116000559886905,0.155009589811987,
1.10659401133715));
#30982=CARTESIAN_POINT('Ctrl Pts',(0.126488220095427,0.147101893720343,
1.10611923196118));
#30983=CARTESIAN_POINT('Ctrl Pts',(0.136144216947772,0.138260857674004,
1.10564559537577));
#30984=CARTESIAN_POINT('Ctrl Pts',(0.143255609150872,0.131749663048667,
1.1052967742678));
#30985=CARTESIAN_POINT('Ctrl Pts',(0.149915772834495,0.124730943289562,
1.10494857300279));
#30986=CARTESIAN_POINT('Ctrl Pts',(0.156057659382849,0.117255425406029,
1.1046));
#30987=CARTESIAN_POINT('',(-0.0999999999999999,-1.22464679914735E-17,1.2));
#30988=CARTESIAN_POINT('',(-0.15,-1.83697019872103E-17,1.15));
#30989=CARTESIAN_POINT('Origin',(0.,0.,1.2));
#30990=CARTESIAN_POINT('Ctrl Pts',(0.113509973994371,-0.159049193030953,
-0.0230074082272069));
#30991=CARTESIAN_POINT('Ctrl Pts',(0.166385127640631,-0.121313337847033,
-0.019303686544359));
#30992=CARTESIAN_POINT('Ctrl Pts',(0.230633516687349,0.0103782615975306,
-0.0118962431786632));
#30993=CARTESIAN_POINT('Ctrl Pts',(0.116188988078006,0.199753850566951,
-0.000785078130119459));
#30994=CARTESIAN_POINT('Ctrl Pts',(-0.104655428901899,0.205782953697956,
0.0103260869184242));
#30995=CARTESIAN_POINT('Ctrl Pts',(-0.229698075471667,0.0238333788527267,
0.0214372519669679));
#30996=CARTESIAN_POINT('Ctrl Pts',(-0.144613108848303,-0.180075271725216,
0.0325484170155115));
#30997=CARTESIAN_POINT('Ctrl Pts',(0.0727946961077783,-0.219149774367173,
0.0436595820640553));
#30998=CARTESIAN_POINT('Ctrl Pts',(0.22359411788162,-0.057762978583554,
0.0547707471125989));
#30999=CARTESIAN_POINT('Ctrl Pts',(0.169827668332871,0.156494259322429,
0.0658819121611427));
#31000=CARTESIAN_POINT('Ctrl Pts',(-0.0393188016825179,0.227560800163251,
0.0769930772096863));
#31001=CARTESIAN_POINT('Ctrl Pts',(-0.212490816724285,0.090434536960108,
0.0881042422582301));
#31002=CARTESIAN_POINT('Ctrl Pts',(-0.19125222930514,-0.129434912039326,
0.0992154073067737));
#31003=CARTESIAN_POINT('Ctrl Pts',(0.00496630258143332,-0.230880650358359,
0.110326572355317));
#31004=CARTESIAN_POINT('Ctrl Pts',(0.196640931676781,-0.121090966106477,
0.121437737403861));
#31005=CARTESIAN_POINT('Ctrl Pts',(0.208405785032279,0.0994871990457256,
0.132548902452405));
#31006=CARTESIAN_POINT('Ctrl Pts',(0.0294968904732024,0.229042728261432,
0.143660067500948));
#31007=CARTESIAN_POINT('Ctrl Pts',(-0.176399147035948,0.149043619583305,
0.154771232549492));
#31008=CARTESIAN_POINT('Ctrl Pts',(-0.220904863824581,-0.0673178902258552,
0.165882397598036));
#31009=CARTESIAN_POINT('Ctrl Pts',(-0.0633012670336293,-0.222089176195486,
0.17699356264658));
#31010=CARTESIAN_POINT('Ctrl Pts',(0.152217643594786,-0.173667627565877,
0.188104727695123));
#31011=CARTESIAN_POINT('Ctrl Pts',(0.228470258285089,0.0336451535954383,
0.199215892743667));
#31012=CARTESIAN_POINT('Ctrl Pts',(0.0956918672404541,0.210175453516431,
0.210327057792211));
#31013=CARTESIAN_POINT('Ctrl Pts',(-0.124636506047609,0.194412953698174,
0.221438222840754));
#31014=CARTESIAN_POINT('Ctrl Pts',(-0.230932995110325,0.000779007092406014,
0.232549387889298));
#31015=CARTESIAN_POINT('Ctrl Pts',(-0.12594528285163,-0.193567664513544,
0.243660552937842));
#31016=CARTESIAN_POINT('Ctrl Pts',(0.0942717341349318,-0.21081625941051,
0.254771717986386));
#31017=CARTESIAN_POINT('Ctrl Pts',(0.228238070382781,-0.0351857683462,0.265882883034929));
#31018=CARTESIAN_POINT('Ctrl Pts',(0.153385834111148,0.172636731182735,
0.276994048083473));
#31019=CARTESIAN_POINT('Ctrl Pts',(-0.0618014955343493,0.222511191222357,
0.288105213132016));
#31020=CARTESIAN_POINT('Ctrl Pts',(-0.220445672440028,0.068806689849701,
0.299216378180561));
#31021=CARTESIAN_POINT('Ctrl Pts',(-0.177400663329184,-0.147850125855229,
0.310327543229104));
#31022=CARTESIAN_POINT('Ctrl Pts',(0.0279509811935462,-0.229236554058792,
0.321438708277648));
#31023=CARTESIAN_POINT('Ctrl Pts',(0.207729836817097,-0.100890881459812,
0.332549873326191));
#31024=CARTESIAN_POINT('Ctrl Pts',(0.197453422882556,0.11976143309821,0.343661038374735));
#31025=CARTESIAN_POINT('Ctrl Pts',(0.00652379087403971,0.230842143506323,
0.354772203423278));
#31026=CARTESIAN_POINT('Ctrl Pts',(-0.190374559216213,0.130721774273047,
0.365883368471823));
#31027=CARTESIAN_POINT('Ctrl Pts',(-0.213096254074054,-0.0889979863001003,
0.376994533520366));
#31028=CARTESIAN_POINT('Ctrl Pts',(-0.0408528604769679,-0.227292100295502,
0.38810569856891));
#31029=CARTESIAN_POINT('Ctrl Pts',(0.16876745272456,-0.15763312458598,0.399216863617453));
#31030=CARTESIAN_POINT('Ctrl Pts',(0.223979789625721,0.0562468568463683,
0.410328028665997));
#31031=CARTESIAN_POINT('Ctrl Pts',(0.0742695215461042,0.218665711155622,
0.421439193714541));
#31032=CARTESIAN_POINT('Ctrl Pts',(-0.143391090854028,0.181023893808443,
0.432550358763085));
#31033=CARTESIAN_POINT('Ctrl Pts',(-0.229860956455329,-0.0222395090620434,
0.443661523811628));
#31034=CARTESIAN_POINT('Ctrl Pts',(-0.106027445761331,-0.205155638019547,
0.454772688860172));
#31035=CARTESIAN_POINT('Ctrl Pts',(0.114812229735204,-0.200371672072451,
0.465883853908716));
#31036=CARTESIAN_POINT('Ctrl Pts',(0.230608404475241,-0.0122645363248325,
0.476995018957259));
#31037=CARTESIAN_POINT('Ctrl Pts',(0.135417351061808,0.187063615108022,
0.488106184005803));
#31038=CARTESIAN_POINT('Ctrl Pts',(-0.083669150175529,0.21524434574405,
0.499217349054346));
#31039=CARTESIAN_POINT('Ctrl Pts',(-0.226205440167697,0.0464946653328952,
0.510328514102891));
#31040=CARTESIAN_POINT('Ctrl Pts',(-0.161782842764492,-0.164793709991974,
0.521439679151433));
#31041=CARTESIAN_POINT('Ctrl Pts',(0.0506574022840452,-0.225309748257175,
0.532550844199978));
#31042=CARTESIAN_POINT('Ctrl Pts',(0.21675039941815,-0.0796863816342033,
0.543662009248521));
#31043=CARTESIAN_POINT('Ctrl Pts',(0.184535073495005,0.138843299139974,
0.554773174297065));
#31044=CARTESIAN_POINT('Ctrl Pts',(-0.01651427104253,0.230343078727826,
0.565884339345609));
#31045=CARTESIAN_POINT('Ctrl Pts',(-0.2024544512798,0.11109838082922,0.576995504394152));
#31046=CARTESIAN_POINT('Ctrl Pts',(-0.203165894515671,-0.109791959503082,
0.588106669442697));
#31047=CARTESIAN_POINT('Ctrl Pts',(-0.0179976902307884,-0.230231922661119,
0.599217834491239));
#31048=CARTESIAN_POINT('Ctrl Pts',(0.183636881720094,-0.140029106752845,
0.610328999539785));
#31049=CARTESIAN_POINT('Ctrl Pts',(0.217259204728728,0.0782885242326115,
0.621440164588326));
#31050=CARTESIAN_POINT('Ctrl Pts',(0.0521076907609949,0.224978762618687,
0.632551329636872));
#31051=CARTESIAN_POINT('Ctrl Pts',(-0.160717962682088,0.16583242004264,
0.643662494685413));
#31052=CARTESIAN_POINT('Ctrl Pts',(-0.226500243885858,-0.0450365916286509,
0.65477365973396));
#31053=CARTESIAN_POINT('Ctrl Pts',(-0.0850539171717745,-0.214700922773088,
0.665884824782501));
#31054=CARTESIAN_POINT('Ctrl Pts',(0.134209565723166,-0.187932029027199,
0.676995989831046));
#31055=CARTESIAN_POINT('Ctrl Pts',(0.230682622449346,0.0107788109627418,
0.68810715487959));
#31056=CARTESIAN_POINT('Ctrl Pts',(0.116100547839306,0.199627948587589,
0.699218319928133));
#31057=CARTESIAN_POINT('Ctrl Pts',(-0.104703729866326,0.205834360634882,
0.710329484976677));
#31058=CARTESIAN_POINT('Ctrl Pts',(-0.229712931099768,0.0237197038645086,
0.721440650025221));
#31059=CARTESIAN_POINT('Ctrl Pts',(-0.144554186745893,-0.180096480143545,
0.732551815073763));
#31060=CARTESIAN_POINT('Ctrl Pts',(0.072859438989827,-0.219139583863915,
0.743662980122308));
#31061=CARTESIAN_POINT('Ctrl Pts',(0.223612826941383,-0.0576884623911715,
0.75477414517085));
#31062=CARTESIAN_POINT('Ctrl Pts',(0.16977934979946,0.156542733614398,0.765885310219396));
#31063=CARTESIAN_POINT('Ctrl Pts',(-0.0393879040694563,0.227550539615811,
0.776996475267938));
#31064=CARTESIAN_POINT('Ctrl Pts',(-0.212518549811472,0.0903688057410859,
0.788107640316484));
#31065=CARTESIAN_POINT('Ctrl Pts',(-0.191212657747833,-0.129492758803799,
0.799218805365025));
#31066=CARTESIAN_POINT('Ctrl Pts',(0.00503667898133586,-0.230879377455661,
0.81032997041357));
#31067=CARTESIAN_POINT('Ctrl Pts',(0.196677879493939,-0.121030850518371,
0.821441135462113));
#31068=CARTESIAN_POINT('Ctrl Pts',(0.208375418707704,0.0995506903268707,
0.832552300510658));
#31069=CARTESIAN_POINT('Ctrl Pts',(0.0294270353677539,0.229051751091564,
0.8436634655592));
#31070=CARTESIAN_POINT('Ctrl Pts',(-0.176444601777748,0.14898978999011,
0.854774630607746));
#31071=CARTESIAN_POINT('Ctrl Pts',(-0.22088431932234,-0.0673852547682493,
0.865885795656288));
#31072=CARTESIAN_POINT('Ctrl Pts',(-0.0632335256349382,-0.22210847899434,
0.876996960704833));
#31073=CARTESIAN_POINT('Ctrl Pts',(0.152270606837662,-0.173621188252162,
0.888108125753376));
#31074=CARTESIAN_POINT('Ctrl Pts',(0.228459985995541,0.0337148347205355,
0.899219290801919));
#31075=CARTESIAN_POINT('Ctrl Pts',(0.0956277562497704,0.210204633917866,
0.910330455850463));
#31076=CARTESIAN_POINT('Ctrl Pts',(-0.12469579560031,0.194374924182257,
0.921441620899007));
#31077=CARTESIAN_POINT('Ctrl Pts',(-0.230933226540692,0.000708579792413808,
0.932552785947551));
#31078=CARTESIAN_POINT('Ctrl Pts',(-0.125886228368054,-0.193606087509586,
0.943663950996094));
#31079=CARTESIAN_POINT('Ctrl Pts',(0.0943360139257667,-0.210787462610152,
0.954775116044639));
#31080=CARTESIAN_POINT('Ctrl Pts',(0.228248823506631,-0.0351162152961091,
0.965886281093181));
#31081=CARTESIAN_POINT('Ctrl Pts',(0.153333110744206,0.172683627576032,
0.976997446141726));
#31082=CARTESIAN_POINT('Ctrl Pts',(-0.0618692454411617,0.222492101746939,
0.988108611190268));
#31083=CARTESIAN_POINT('Ctrl Pts',(-0.220466868021367,0.0687398848825245,
0.999219776238814));
#31084=CARTESIAN_POINT('Ctrl Pts',(-0.17735514221838,-0.147905058047522,
1.01033094128735));
#31085=CARTESIAN_POINT('Ctrl Pts',(0.0280201048116106,-0.229226437530741,
1.0214421063359));
#31086=CARTESIAN_POINT('Ctrl Pts',(0.207762111854432,-0.10083052618152,
1.03255327138444));
#31087=CARTESIAN_POINT('Ctrl Pts',(0.197414006873683,0.119827380577986,
1.04366443643299));
#31088=CARTESIAN_POINT('Ctrl Pts',(0.00645886152005097,0.230833217918201,
1.05477560148153));
#31089=CARTESIAN_POINT('Ctrl Pts',(-0.190424854748374,0.130684465150768,
1.06588676653008));
#31090=CARTESIAN_POINT('Ctrl Pts',(-0.213049227679005,-0.0891025387309722,
1.07699793157862));
#31091=CARTESIAN_POINT('Ctrl Pts',(-0.0408214485225542,-0.227228942196666,
1.08810909662716));
#31092=CARTESIAN_POINT('Ctrl Pts',(0.168888461736298,-0.15772814986318,
1.09922026167571));
#31093=CARTESIAN_POINT('Ctrl Pts',(0.223817187934597,0.0566161966084782,
1.11033142672425));
#31094=CARTESIAN_POINT('Ctrl Pts',(0.124300218570944,0.164165746435707,
1.11773887008995));
#31095=CARTESIAN_POINT('Ctrl Pts',(0.0627850911123727,0.1850383536838,1.12144259177279));
#31096=CARTESIAN_POINT('Ctrl Pts',(0.105793541951254,-0.14823699524473,
-0.0153382721514713));
#31097=CARTESIAN_POINT('Ctrl Pts',(0.155074231467859,-0.113066431478549,
-0.0116345504686234));
#31098=CARTESIAN_POINT('Ctrl Pts',(0.214955001436596,0.00967274517879857,
-0.00422710710292769));
#31099=CARTESIAN_POINT('Ctrl Pts',(0.108290436090784,0.186174541551099,
0.00688405794561606));
#31100=CARTESIAN_POINT('Ctrl Pts',(-0.0975409307071879,0.191793784975909,
0.0179952229941597));
#31101=CARTESIAN_POINT('Ctrl Pts',(-0.214083151712633,0.022213180716797,
0.0291063880427034));
#31102=CARTESIAN_POINT('Ctrl Pts',(-0.134782279118508,-0.167833716661673,
0.0402175530912472));
#31103=CARTESIAN_POINT('Ctrl Pts',(0.0678460972679723,-0.204251926348524,
0.0513287181397908));
#31104=CARTESIAN_POINT('Ctrl Pts',(0.208394142450739,-0.0538362390807298,
0.0624398831883346));
#31105=CARTESIAN_POINT('Ctrl Pts',(0.158282747515632,0.145855746470163,
0.0735510482368781));
#31106=CARTESIAN_POINT('Ctrl Pts',(-0.0366459012269607,0.212091168831785,
0.084662213285422));
#31107=CARTESIAN_POINT('Ctrl Pts',(-0.198045646054783,0.0842867780077688,
0.0957733783339656));
#31108=CARTESIAN_POINT('Ctrl Pts',(-0.178250862301028,-0.120635899339281,
0.106884543382509));
#31109=CARTESIAN_POINT('Ctrl Pts',(0.00462869228141735,-0.215185334908375,
0.117995708431053));
#31110=CARTESIAN_POINT('Ctrl Pts',(0.183273239545565,-0.112859176615955,
0.129106873479597));
#31111=CARTESIAN_POINT('Ctrl Pts',(0.194238315681312,0.0927240382098824,
0.14021803852814));
#31112=CARTESIAN_POINT('Ctrl Pts',(0.0274916856192995,0.213472355144377,
0.151329203576684));
#31113=CARTESIAN_POINT('Ctrl Pts',(-0.164407495706399,0.138911602796551,
0.162440368625228));
#31114=CARTESIAN_POINT('Ctrl Pts',(-0.20588770445336,-0.062741605808422,
0.173551533673771));
#31115=CARTESIAN_POINT('Ctrl Pts',(-0.0589980335104445,-0.206991507018771,
0.184662698722315));
#31116=CARTESIAN_POINT('Ctrl Pts',(0.141869855984326,-0.161861665507704,
0.195773863770859));
#31117=CARTESIAN_POINT('Ctrl Pts',(0.21293880179812,0.0313579489369987,
0.206885028819403));
#31118=CARTESIAN_POINT('Ctrl Pts',(0.0891867138635642,0.195887681727571,
0.217996193867946));
#31119=CARTESIAN_POINT('Ctrl Pts',(-0.116163690001897,0.18119671998123,
0.22910735891649));
#31120=CARTESIAN_POINT('Ctrl Pts',(-0.21523412125303,0.00072605002547781,
0.240218523965033));
#31121=CARTESIAN_POINT('Ctrl Pts',(-0.11738349588193,-0.180408893734178,
0.251329689013577));
#31122=CARTESIAN_POINT('Ctrl Pts',(0.0878631217069615,-0.196484925501419,
0.262440854062121));
#31123=CARTESIAN_POINT('Ctrl Pts',(0.212722398078527,-0.0327938323711113,
0.273552019110664));
#31124=CARTESIAN_POINT('Ctrl Pts',(0.142958632662274,0.160900849678758,
0.284663184159209));
#31125=CARTESIAN_POINT('Ctrl Pts',(-0.057600216794938,0.207384833374845,
0.295774349207752));
#31126=CARTESIAN_POINT('Ctrl Pts',(-0.205459728996263,0.0641291965189069,
0.306885514256296));
#31127=CARTESIAN_POINT('Ctrl Pts',(-0.165340928710165,-0.137799243024573,
0.317996679304839));
#31128=CARTESIAN_POINT('Ctrl Pts',(0.0260508675794864,-0.213653004623031,
0.329107844353384));
#31129=CARTESIAN_POINT('Ctrl Pts',(0.193608318568785,-0.0940322979965331,
0.340219009401926));
#31130=CARTESIAN_POINT('Ctrl Pts',(0.184030497427301,0.111620025542831,
0.351330174450471));
#31131=CARTESIAN_POINT('Ctrl Pts',(0.00608030219043116,0.215149445760286,
0.362441339499014));
#31132=CARTESIAN_POINT('Ctrl Pts',(-0.177432856410404,0.121835280406139,
0.373552504547559));
#31133=CARTESIAN_POINT('Ctrl Pts',(-0.198609925645444,-0.0829478843655077,
0.384663669596101));
#31134=CARTESIAN_POINT('Ctrl Pts',(-0.0380756743800589,-0.211840735237885,
0.395774834644646));
#31135=CARTESIAN_POINT('Ctrl Pts',(0.157294605588646,-0.14691719143219,
0.406885999693188));
#31136=CARTESIAN_POINT('Ctrl Pts',(0.208753596148093,0.0524231836199493,
0.417997164741733));
#31137=CARTESIAN_POINT('Ctrl Pts',(0.0692206637610257,0.203800769856489,
0.429108329790276));
#31138=CARTESIAN_POINT('Ctrl Pts',(-0.133643334165982,0.168717851215016,
0.44021949483882));
#31139=CARTESIAN_POINT('Ctrl Pts',(-0.21423496001257,-0.0207276625316418,
0.451330659887364));
#31140=CARTESIAN_POINT('Ctrl Pts',(-0.0988196775702872,-0.191209114350017,
0.462441824935908));
#31141=CARTESIAN_POINT('Ctrl Pts',(0.107007270071357,-0.186750363419964,
0.473552989984451));
#31142=CARTESIAN_POINT('Ctrl Pts',(0.21493159635798,-0.011430790551128,
0.484664155032995));
#31143=CARTESIAN_POINT('Ctrl Pts',(0.126211650891535,0.174346990983058,
0.495775320081538));
#31144=CARTESIAN_POINT('Ctrl Pts',(-0.0779813036479037,0.200611989589323,
0.506886485130082));
#31145=CARTESIAN_POINT('Ctrl Pts',(-0.21082794649543,0.0433339481484583,
0.517997650178626));
#31146=CARTESIAN_POINT('Ctrl Pts',(-0.150784810891129,-0.153590998727594,
0.529108815227169));
#31147=CARTESIAN_POINT('Ctrl Pts',(0.0472137013611209,-0.209993143910453,
0.540219980275713));
#31148=CARTESIAN_POINT('Ctrl Pts',(0.202015661416081,-0.0742692845544967,
0.551331145324257));
#31149=CARTESIAN_POINT('Ctrl Pts',(0.171990340163759,0.129404702294652,
0.562442310372801));
#31150=CARTESIAN_POINT('Ctrl Pts',(-0.0153916274037652,0.214684307510999,
0.573553475421344));
#31151=CARTESIAN_POINT('Ctrl Pts',(-0.188691554856225,0.103545889399597,
0.584664640469888));
#31152=CARTESIAN_POINT('Ctrl Pts',(-0.189354634030427,-0.102328278871562,
0.595775805518432));
#31153=CARTESIAN_POINT('Ctrl Pts',(-0.0167742034418123,-0.21458070785722,
0.606886970566975));
#31154=CARTESIAN_POINT('Ctrl Pts',(0.171153207655705,-0.130509898455162,
0.61799813561552));
#31155=CARTESIAN_POINT('Ctrl Pts',(0.202489878034016,0.0729664537947597,
0.629109300664062));
#31156=CARTESIAN_POINT('Ctrl Pts',(0.0485653989206222,0.209684658745684,
0.640220465712607));
#31157=CARTESIAN_POINT('Ctrl Pts',(-0.149792321581985,0.154559097049293,
0.65133163076115));
#31158=CARTESIAN_POINT('Ctrl Pts',(-0.211102709394471,-0.041974994603061,
0.662442795809694));
#31159=CARTESIAN_POINT('Ctrl Pts',(-0.079271933890819,-0.20010550862688,
0.673553960858237));
#31160=CARTESIAN_POINT('Ctrl Pts',(0.125085971055702,-0.17515636994031,
0.684665125906781));
#31161=CARTESIAN_POINT('Ctrl Pts',(0.215000768978506,0.0100460651134341,
0.695776290955325));
#31162=CARTESIAN_POINT('Ctrl Pts',(0.108208008038219,0.186057198414926,
0.706887456003868));
#31163=CARTESIAN_POINT('Ctrl Pts',(-0.0975859481618359,0.191841697258389,
0.717998621052413));
#31164=CARTESIAN_POINT('Ctrl Pts',(-0.214096997451993,0.0221072333783236,
0.729109786100956));
#31165=CARTESIAN_POINT('Ctrl Pts',(-0.134727362553083,-0.167853483327237,
0.7402209511495));
#31166=CARTESIAN_POINT('Ctrl Pts',(0.0679064389152043,-0.204242428597833,
0.751332116198043));
#31167=CARTESIAN_POINT('Ctrl Pts',(0.208411579664662,-0.0537667885148679,
0.762443281246587));
#31168=CARTESIAN_POINT('Ctrl Pts',(0.158237713686343,0.14590092546951,0.773554446295131));
#31169=CARTESIAN_POINT('Ctrl Pts',(-0.0367103060190181,0.21208160579853,
0.784665611343674));
#31170=CARTESIAN_POINT('Ctrl Pts',(-0.198071493840836,0.0842255152109201,
0.795776776392219));
#31171=CARTESIAN_POINT('Ctrl Pts',(-0.178213980826558,-0.120689813668469,
0.80688794144076));
#31172=CARTESIAN_POINT('Ctrl Pts',(0.00469428447876819,-0.215184148537872,
0.817999106489307));
#31173=CARTESIAN_POINT('Ctrl Pts',(0.183307675642296,-0.112803147698245,
0.829110271537848));
#31174=CARTESIAN_POINT('Ctrl Pts',(0.194210013665906,0.0927832133403047,
0.840221436586394));
#31175=CARTESIAN_POINT('Ctrl Pts',(0.0274265792786954,0.213480764600607,
0.851332601634936));
#31176=CARTESIAN_POINT('Ctrl Pts',(-0.164449860425235,0.138861432550488,
0.86244376668348));
#31177=CARTESIAN_POINT('Ctrl Pts',(-0.205868556570727,-0.0628043908949741,
0.873554931732024));
#31178=CARTESIAN_POINT('Ctrl Pts',(-0.0589348971863656,-0.207009497609277,
0.884666096780567));
#31179=CARTESIAN_POINT('Ctrl Pts',(0.141919218774748,-0.161818383148359,
0.895777261829112));
#31180=CARTESIAN_POINT('Ctrl Pts',(0.212929227820989,0.0314228931244718,
0.906888426877654));
#31181=CARTESIAN_POINT('Ctrl Pts',(0.0891269611515884,0.195914878439144,
0.9179995919262));
#31182=CARTESIAN_POINT('Ctrl Pts',(-0.116218949038264,0.181161275719849,
0.929110756974741));
#31183=CARTESIAN_POINT('Ctrl Pts',(-0.215234336950711,0.000660410388236847,
0.940221922023287));
#31184=CARTESIAN_POINT('Ctrl Pts',(-0.117328455934639,-0.180444704726821,
0.951333087071829));
#31185=CARTESIAN_POINT('Ctrl Pts',(0.0879230317440182,-0.196458086313641,
0.962444252120374));
#31186=CARTESIAN_POINT('Ctrl Pts',(0.212732420202743,-0.0327290075520782,
0.973555417168917));
#31187=CARTESIAN_POINT('Ctrl Pts',(0.142909493440969,0.160944558045319,
0.98466658221746));
#31188=CARTESIAN_POINT('Ctrl Pts',(-0.0576633610487541,0.207367041606005,
0.995777747266004));
#31189=CARTESIAN_POINT('Ctrl Pts',(-0.205479483697499,0.0640669329675303,
1.00688891231455));
#31190=CARTESIAN_POINT('Ctrl Pts',(-0.165298502134104,-0.137850440914814,
1.01800007736309));
#31191=CARTESIAN_POINT('Ctrl Pts',(0.026115292159373,-0.213643575818697,
1.02911124241164));
#31192=CARTESIAN_POINT('Ctrl Pts',(0.193638399542254,-0.0939760456828254,
1.04022240746018));
#31193=CARTESIAN_POINT('Ctrl Pts',(0.183993760927049,0.111681489898982,
1.05133357250872));
#31194=CARTESIAN_POINT('Ctrl Pts',(0.00601978674766102,0.215141126935532,
1.06244473755726));
#31195=CARTESIAN_POINT('Ctrl Pts',(-0.177479732841649,0.121800507565884,
1.07355590260581));
#31196=CARTESIAN_POINT('Ctrl Pts',(-0.198566096114678,-0.0830453293000129,
1.08466706765435));
#31197=CARTESIAN_POINT('Ctrl Pts',(-0.0380463978169507,-0.211781870639967,
1.0957782327029));
#31198=CARTESIAN_POINT('Ctrl Pts',(0.157407388382168,-0.147005756870945,
1.10688939775144));
#31199=CARTESIAN_POINT('Ctrl Pts',(0.208602048154327,0.0527674155869038,
1.11800056279999));
#31200=CARTESIAN_POINT('Ctrl Pts',(0.115850263419028,0.153005724266717,
1.12540800616568));
#31201=CARTESIAN_POINT('Ctrl Pts',(0.0585169473375027,0.172459407258861,
1.12911172784853));
#31202=CARTESIAN_POINT('Ctrl Pts',(0.0980771099081375,-0.137424797458507,
-0.00766913607573581));
#31203=CARTESIAN_POINT('Ctrl Pts',(0.143763335295088,-0.104819525110066,
-0.00396541439288791));
#31204=CARTESIAN_POINT('Ctrl Pts',(0.199276486185844,0.0089672287600667,
0.00344202897280782));
#31205=CARTESIAN_POINT('Ctrl Pts',(0.100391884103562,0.172595232535247,
0.0145531940213516));
#31206=CARTESIAN_POINT('Ctrl Pts',(-0.0904264325124765,0.177804616253862,
0.0256643590698952));
#31207=CARTESIAN_POINT('Ctrl Pts',(-0.198468227953599,0.020592982580867,
0.036775524118439));
#31208=CARTESIAN_POINT('Ctrl Pts',(-0.124951449388714,-0.155592161598129,
0.0478866891669827));
#31209=CARTESIAN_POINT('Ctrl Pts',(0.0628974984281669,-0.189354078329874,
0.0589978542155263));
#31210=CARTESIAN_POINT('Ctrl Pts',(0.193194167019859,-0.0499094995779056,
0.07010901926407));
#31211=CARTESIAN_POINT('Ctrl Pts',(0.146737826698393,0.135217233617898,
0.0812201843126137));
#31212=CARTESIAN_POINT('Ctrl Pts',(-0.0339730007714042,0.196621537500318,
0.0923313493611574));
#31213=CARTESIAN_POINT('Ctrl Pts',(-0.18360047538528,0.07813901905543,0.103442514409701));
#31214=CARTESIAN_POINT('Ctrl Pts',(-0.165249495296916,-0.111836886639236,
0.114553679458245));
#31215=CARTESIAN_POINT('Ctrl Pts',(0.00429108198140191,-0.199490019458391,
0.125664844506789));
#31216=CARTESIAN_POINT('Ctrl Pts',(0.169905547414348,-0.104627387125433,
0.136776009555332));
#31217=CARTESIAN_POINT('Ctrl Pts',(0.180070846330345,0.0859608773740392,
0.147887174603876));
#31218=CARTESIAN_POINT('Ctrl Pts',(0.0254864807653961,0.197901982027321,
0.15899833965242));
#31219=CARTESIAN_POINT('Ctrl Pts',(-0.152415844376849,0.128779586009797,
0.170109504700963));
#31220=CARTESIAN_POINT('Ctrl Pts',(-0.190870545082139,-0.0581653213909888,
0.181220669749507));
#31221=CARTESIAN_POINT('Ctrl Pts',(-0.0546947999872595,-0.191893837842057,
0.192331834798051));
#31222=CARTESIAN_POINT('Ctrl Pts',(0.131522068373867,-0.150055703449532,
0.203442999846594));
#31223=CARTESIAN_POINT('Ctrl Pts',(0.197407345311151,0.0290707442785592,
0.214554164895138));
#31224=CARTESIAN_POINT('Ctrl Pts',(0.0826815604866742,0.181599909938712,
0.225665329943681));
#31225=CARTESIAN_POINT('Ctrl Pts',(-0.107690873956185,0.167980486264285,
0.236776494992226));
#31226=CARTESIAN_POINT('Ctrl Pts',(-0.199535247395734,0.000673092958549589,
0.247887660040769));
#31227=CARTESIAN_POINT('Ctrl Pts',(-0.10882170891223,-0.167250122954812,
0.258998825089313));
#31228=CARTESIAN_POINT('Ctrl Pts',(0.0814545092789914,-0.182153591592328,
0.270109990137857));
#31229=CARTESIAN_POINT('Ctrl Pts',(0.197206725774273,-0.0304018963960226,
0.2812211551864));
#31230=CARTESIAN_POINT('Ctrl Pts',(0.1325314312134,0.149164968174781,0.292332320234944));
#31231=CARTESIAN_POINT('Ctrl Pts',(-0.0533989380555266,0.192258475527334,
0.303443485283487));
#31232=CARTESIAN_POINT('Ctrl Pts',(-0.190473785552499,0.0594517031881129,
0.314554650332031));
#31233=CARTESIAN_POINT('Ctrl Pts',(-0.153281194091147,-0.127748360193918,
0.325665815380575));
#31234=CARTESIAN_POINT('Ctrl Pts',(0.0241507539654265,-0.198069455187271,
0.336776980429119));
#31235=CARTESIAN_POINT('Ctrl Pts',(0.179486800320472,-0.0871737145332536,
0.347888145477662));
#31236=CARTESIAN_POINT('Ctrl Pts',(0.170607571972046,0.103478617987453,
0.358999310526206));
#31237=CARTESIAN_POINT('Ctrl Pts',(0.00563681350682242,0.199456748014249,
0.37011047557475));
#31238=CARTESIAN_POINT('Ctrl Pts',(-0.164491153604594,0.11294878653923,
0.381221640623293));
#31239=CARTESIAN_POINT('Ctrl Pts',(-0.184123597216834,-0.0768977824309152,
0.392332805671837));
#31240=CARTESIAN_POINT('Ctrl Pts',(-0.0352984882831497,-0.196389370180267,
0.403443970720381));
#31241=CARTESIAN_POINT('Ctrl Pts',(0.145821758452731,-0.136201258278399,
0.414555135768924));
#31242=CARTESIAN_POINT('Ctrl Pts',(0.193527402670466,0.0485995103935303,
0.425666300817468));
#31243=CARTESIAN_POINT('Ctrl Pts',(0.0641718059759468,0.188935828557357,
0.436777465866012));
#31244=CARTESIAN_POINT('Ctrl Pts',(-0.123895577477937,0.156411808621589,
0.447888630914555));
#31245=CARTESIAN_POINT('Ctrl Pts',(-0.198608963569812,-0.01921581600124,
0.458999795963099));
#31246=CARTESIAN_POINT('Ctrl Pts',(-0.0916119093792434,-0.177262590680487,
0.470110961011643));
#31247=CARTESIAN_POINT('Ctrl Pts',(0.0992023104075105,-0.173129054767478,
0.481222126060186));
#31248=CARTESIAN_POINT('Ctrl Pts',(0.199254788240719,-0.0105970447774237,
0.49233329110873));
#31249=CARTESIAN_POINT('Ctrl Pts',(0.117005950721263,0.161630366858093,
0.503444456157274));
#31250=CARTESIAN_POINT('Ctrl Pts',(-0.0722934571202785,0.185979633434597,
0.514555621205818));
#31251=CARTESIAN_POINT('Ctrl Pts',(-0.195450452823164,0.0401732309640217,
0.525666786254361));
#31252=CARTESIAN_POINT('Ctrl Pts',(-0.139786779017765,-0.142388287463214,
0.536777951302905));
#31253=CARTESIAN_POINT('Ctrl Pts',(0.0437700004381964,-0.19467653956373,
0.547889116351449));
#31254=CARTESIAN_POINT('Ctrl Pts',(0.187280923414012,-0.0688521874747905,
0.559000281399993));
#31255=CARTESIAN_POINT('Ctrl Pts',(0.159445606832513,0.119966105449332,
0.570111446448536));
#31256=CARTESIAN_POINT('Ctrl Pts',(-0.0142689837650004,0.199025536294172,
0.581222611497081));
#31257=CARTESIAN_POINT('Ctrl Pts',(-0.174928658432651,0.0959933979699734,
0.592333776545623));
#31258=CARTESIAN_POINT('Ctrl Pts',(-0.175543373545183,-0.0948645982400418,
0.603444941594168));
#31259=CARTESIAN_POINT('Ctrl Pts',(-0.0155507166528361,-0.198929493053321,
0.61455610664271));
#31260=CARTESIAN_POINT('Ctrl Pts',(0.158669533591315,-0.120990690157479,
0.625667271691256));
#31261=CARTESIAN_POINT('Ctrl Pts',(0.187720551339304,0.0676443833569079,
0.636778436739797));
#31262=CARTESIAN_POINT('Ctrl Pts',(0.0450231070802491,0.194390554872681,
0.647889601788343));
#31263=CARTESIAN_POINT('Ctrl Pts',(-0.138866680481881,0.143285774055946,
0.659000766836885));
#31264=CARTESIAN_POINT('Ctrl Pts',(-0.195705174903083,-0.038913397577471,
0.67011193188543));
#31265=CARTESIAN_POINT('Ctrl Pts',(-0.0734899506098636,-0.185510094480672,
0.681223096933973));
#31266=CARTESIAN_POINT('Ctrl Pts',(0.115962376388238,-0.162380710853421,
0.692334261982516));
#31267=CARTESIAN_POINT('Ctrl Pts',(0.199318915507666,0.00931331926412601,
0.703445427031061));
#31268=CARTESIAN_POINT('Ctrl Pts',(0.100315468237132,0.172486448242263,
0.714556592079604));
#31269=CARTESIAN_POINT('Ctrl Pts',(-0.0904681664573454,0.177849033881895,
0.725667757128148));
#31270=CARTESIAN_POINT('Ctrl Pts',(-0.198481063804218,0.0204947628921387,
0.736778922176691));
#31271=CARTESIAN_POINT('Ctrl Pts',(-0.124900538360275,-0.155610486510929,
0.747890087225236));
#31272=CARTESIAN_POINT('Ctrl Pts',(0.0629534388405818,-0.189345273331751,
0.759001252273779));
#31273=CARTESIAN_POINT('Ctrl Pts',(0.193210332387941,-0.0498451146385645,
0.770112417322323));
#31274=CARTESIAN_POINT('Ctrl Pts',(0.146696077573226,0.135259117324623,
0.781223582370866));
#31275=CARTESIAN_POINT('Ctrl Pts',(-0.0340327079685797,0.196612671981249,
0.79233474741941));
#31276=CARTESIAN_POINT('Ctrl Pts',(-0.1836244378702,0.0780822246807544,
0.803445912467955));
#31277=CARTESIAN_POINT('Ctrl Pts',(-0.165215303905282,-0.111886868533138,
0.814557077516496));
#31278=CARTESIAN_POINT('Ctrl Pts',(0.00435188997620014,-0.199488919620082,
0.825668242565042));
#31279=CARTESIAN_POINT('Ctrl Pts',(0.169937471790653,-0.104575444878119,
0.836779407613584));
#31280=CARTESIAN_POINT('Ctrl Pts',(0.180044608624107,0.0860157363537389,
0.847890572662129));
#31281=CARTESIAN_POINT('Ctrl Pts',(0.0254261231896373,0.197909778109651,
0.859001737710672));
#31282=CARTESIAN_POINT('Ctrl Pts',(-0.152455119072723,0.128733075110866,
0.870112902759215));
#31283=CARTESIAN_POINT('Ctrl Pts',(-0.190852793819114,-0.058223527021699,
0.88122406780776));
#31284=CARTESIAN_POINT('Ctrl Pts',(-0.0546362687377931,-0.191910516224214,
0.892335232856302));
#31285=CARTESIAN_POINT('Ctrl Pts',(0.131567830711834,-0.150015578044556,
0.903446397904849));
#31286=CARTESIAN_POINT('Ctrl Pts',(0.197398469646436,0.0291309515284085,
0.914557562953389));
#31287=CARTESIAN_POINT('Ctrl Pts',(0.0826261660534066,0.181625122960423,
0.925668728001935));
#31288=CARTESIAN_POINT('Ctrl Pts',(-0.107742102476217,0.167947627257441,
0.936779893050478));
#31289=CARTESIAN_POINT('Ctrl Pts',(-0.199535447360731,0.000612240984059651,
0.947891058099021));
#31290=CARTESIAN_POINT('Ctrl Pts',(-0.108770683501224,-0.167283321944057,
0.959002223147566));
#31291=CARTESIAN_POINT('Ctrl Pts',(0.0815100495622697,-0.182128710017129,
0.970113388196108));
#31292=CARTESIAN_POINT('Ctrl Pts',(0.197216016898856,-0.0303417998080474,
0.981224553244654));
#31293=CARTESIAN_POINT('Ctrl Pts',(0.132485876137733,0.149205488514605,
0.992335718293196));
#31294=CARTESIAN_POINT('Ctrl Pts',(-0.0534574766563464,0.19224198146507,
1.00344688334174));
#31295=CARTESIAN_POINT('Ctrl Pts',(-0.190492099373632,0.0593939810525364,
1.01455804839028));
#31296=CARTESIAN_POINT('Ctrl Pts',(-0.153241862049827,-0.127795823782107,
1.02566921343883));
#31297=CARTESIAN_POINT('Ctrl Pts',(0.0242104795071353,-0.198060714106653,
1.03678037848737));
#31298=CARTESIAN_POINT('Ctrl Pts',(0.179514687230076,-0.0871215651841315,
1.04789154353591));
#31299=CARTESIAN_POINT('Ctrl Pts',(0.170573514980415,0.103535599219979,
1.05900270858446));
#31300=CARTESIAN_POINT('Ctrl Pts',(0.0055807119752709,0.199449035952863,
1.070113873633));
#31301=CARTESIAN_POINT('Ctrl Pts',(-0.164534610934924,0.112916549981001,
1.08122503868155));
#31302=CARTESIAN_POINT('Ctrl Pts',(-0.184082964550351,-0.0769881198690536,
1.09233620373009));
#31303=CARTESIAN_POINT('Ctrl Pts',(-0.0352713471113472,-0.196334799083268,
1.10344736877863));
#31304=CARTESIAN_POINT('Ctrl Pts',(0.145926315028038,-0.136283363878709,
1.11455853382718));
#31305=CARTESIAN_POINT('Ctrl Pts',(0.193386908374058,0.0489186345653294,
1.12566969887572));
#31306=CARTESIAN_POINT('Ctrl Pts',(0.107400308267113,0.141845702097726,
1.13307714224142));
#31307=CARTESIAN_POINT('Ctrl Pts',(0.0542488035626326,0.159880460833922,
1.13678086392426));
#31308=CARTESIAN_POINT('Ctrl Pts',(0.0903606778650208,-0.126612599672284,
-2.77555756156289E-16));
#31309=CARTESIAN_POINT('Ctrl Pts',(0.132452439122316,-0.0965726187415828,
0.00370372168284762));
#31310=CARTESIAN_POINT('Ctrl Pts',(0.183597970935092,0.00826171234133487,
0.0111111650485434));
#31311=CARTESIAN_POINT('Ctrl Pts',(0.0924933321163406,0.159015923519395,
0.0222223300970871));
#31312=CARTESIAN_POINT('Ctrl Pts',(-0.0833119343177651,0.163815447531815,
0.0333334951456308));
#31313=CARTESIAN_POINT('Ctrl Pts',(-0.182853304194564,0.018972784444937,
0.0444446601941745));
#31314=CARTESIAN_POINT('Ctrl Pts',(-0.115120619658919,-0.143350606534586,
0.0555558252427182));
#31315=CARTESIAN_POINT('Ctrl Pts',(0.0579488995883613,-0.174456230311225,
0.0666669902912619));
#31316=CARTESIAN_POINT('Ctrl Pts',(0.177994191588978,-0.0459827600750814,
0.0777781553398056));
#31317=CARTESIAN_POINT('Ctrl Pts',(0.135192905881154,0.124578720765632,
0.0888893203883492));
#31318=CARTESIAN_POINT('Ctrl Pts',(-0.0313001003158473,0.181151906168851,
0.100000485436893));
#31319=CARTESIAN_POINT('Ctrl Pts',(-0.169155304715778,0.0719912601030908,
0.111111650485437));
#31320=CARTESIAN_POINT('Ctrl Pts',(-0.152248128292804,-0.103037873939191,
0.12222281553398));
#31321=CARTESIAN_POINT('Ctrl Pts',(0.00395347168138628,-0.183794704008407,
0.133333980582524));
#31322=CARTESIAN_POINT('Ctrl Pts',(0.156537855283131,-0.0963955976349113,
0.144445145631068));
#31323=CARTESIAN_POINT('Ctrl Pts',(0.165903376979378,0.0791977165381959,
0.155556310679611));
#31324=CARTESIAN_POINT('Ctrl Pts',(0.0234812759114929,0.182331608910266,
0.166667475728155));
#31325=CARTESIAN_POINT('Ctrl Pts',(-0.1404241930473,0.118647569223042,0.177778640776699));
#31326=CARTESIAN_POINT('Ctrl Pts',(-0.175853385710917,-0.0535890369735552,
0.188889805825242));
#31327=CARTESIAN_POINT('Ctrl Pts',(-0.0503915664640746,-0.176796168665343,
0.200000970873786));
#31328=CARTESIAN_POINT('Ctrl Pts',(0.121174280763407,-0.138249741391359,
0.21111213592233));
#31329=CARTESIAN_POINT('Ctrl Pts',(0.181875888824183,0.0267835396201195,
0.222223300970874));
#31330=CARTESIAN_POINT('Ctrl Pts',(0.0761764071097843,0.167312138149853,
0.233334466019417));
#31331=CARTESIAN_POINT('Ctrl Pts',(-0.0992180579104728,0.154764252547341,
0.244445631067961));
#31332=CARTESIAN_POINT('Ctrl Pts',(-0.183836373538439,0.000620135891621234,
0.255556796116504));
#31333=CARTESIAN_POINT('Ctrl Pts',(-0.10025992194253,-0.154091352175446,
0.266667961165049));
#31334=CARTESIAN_POINT('Ctrl Pts',(0.0750458968510211,-0.167822257683237,
0.277779126213592));
#31335=CARTESIAN_POINT('Ctrl Pts',(0.181691053470019,-0.0280099604209337,
0.288890291262136));
#31336=CARTESIAN_POINT('Ctrl Pts',(0.122104229764526,0.137429086670804,
0.30000145631068));
#31337=CARTESIAN_POINT('Ctrl Pts',(-0.0491976593161155,0.177132117679823,
0.311112621359223));
#31338=CARTESIAN_POINT('Ctrl Pts',(-0.175487842108734,0.0547742098573187,
0.322223786407767));
#31339=CARTESIAN_POINT('Ctrl Pts',(-0.141221459472129,-0.117697477363263,
0.33333495145631));
#31340=CARTESIAN_POINT('Ctrl Pts',(0.0222506403513669,-0.18248590575151,
0.344446116504855));
#31341=CARTESIAN_POINT('Ctrl Pts',(0.165365282072159,-0.0803151310699741,
0.355557281553397));
#31342=CARTESIAN_POINT('Ctrl Pts',(0.157184646516792,0.0953372104320743,
0.366668446601942));
#31343=CARTESIAN_POINT('Ctrl Pts',(0.00519332482321354,0.183764050268212,
0.377779611650485));
#31344=CARTESIAN_POINT('Ctrl Pts',(-0.151549450798785,0.104062292672322,
0.388890776699029));
#31345=CARTESIAN_POINT('Ctrl Pts',(-0.169637268788223,-0.0708476804963227,
0.400001941747572));
#31346=CARTESIAN_POINT('Ctrl Pts',(-0.0325213021862407,-0.180938005122649,
0.411113106796117));
#31347=CARTESIAN_POINT('Ctrl Pts',(0.134348911316817,-0.125485325124609,
0.42222427184466));
#31348=CARTESIAN_POINT('Ctrl Pts',(0.178301209192838,0.0447758371671112,
0.433335436893204));
#31349=CARTESIAN_POINT('Ctrl Pts',(0.0591229481908682,0.174070887258225,
0.444446601941748));
#31350=CARTESIAN_POINT('Ctrl Pts',(-0.114147820789891,0.144105766028162,
0.455557766990291));
#31351=CARTESIAN_POINT('Ctrl Pts',(-0.182982967127054,-0.0177039694708382,
0.466668932038835));
#31352=CARTESIAN_POINT('Ctrl Pts',(-0.0844041411881997,-0.163316067010957,
0.477780097087378));
#31353=CARTESIAN_POINT('Ctrl Pts',(0.0913973507436636,-0.159507746114991,
0.488891262135923));
#31354=CARTESIAN_POINT('Ctrl Pts',(0.183577980123458,-0.00976329900371924,
0.500002427184466));
#31355=CARTESIAN_POINT('Ctrl Pts',(0.10780025055099,0.148913742733129,0.51111359223301));
#31356=CARTESIAN_POINT('Ctrl Pts',(-0.0666056105926533,0.17134727727987,
0.522224757281553));
#31357=CARTESIAN_POINT('Ctrl Pts',(-0.180072959150898,0.037012513779585,
0.533335922330097));
#31358=CARTESIAN_POINT('Ctrl Pts',(-0.128788747144402,-0.131185576198834,
0.544447087378641));
#31359=CARTESIAN_POINT('Ctrl Pts',(0.0403262995152723,-0.179359935217008,
0.555558252427184));
#31360=CARTESIAN_POINT('Ctrl Pts',(0.172546185411942,-0.0634350903950841,
0.566669417475728));
#31361=CARTESIAN_POINT('Ctrl Pts',(0.146900873501267,0.11052750860401,0.577780582524271));
#31362=CARTESIAN_POINT('Ctrl Pts',(-0.013146340126236,0.183366765077345,
0.588891747572816));
#31363=CARTESIAN_POINT('Ctrl Pts',(-0.161165762009075,0.0884409065403499,
0.600002912621358));
#31364=CARTESIAN_POINT('Ctrl Pts',(-0.16173211305994,-0.087400917608522,
0.611114077669903));
#31365=CARTESIAN_POINT('Ctrl Pts',(-0.0143272298638598,-0.183278278249422,
0.622225242718446));
#31366=CARTESIAN_POINT('Ctrl Pts',(0.146185859526926,-0.111471481859797,
0.63333640776699));
#31367=CARTESIAN_POINT('Ctrl Pts',(0.172951224644592,0.0623223129190563,
0.644447572815534));
#31368=CARTESIAN_POINT('Ctrl Pts',(0.0414808152398764,0.179096450999678,
0.655558737864077));
#31369=CARTESIAN_POINT('Ctrl Pts',(-0.127941039381778,0.1320124510626,0.666669902912621));
#31370=CARTESIAN_POINT('Ctrl Pts',(-0.180307640411694,-0.0358518005518811,
0.677781067961165));
#31371=CARTESIAN_POINT('Ctrl Pts',(-0.0677079673289082,-0.170914680334463,
0.68889223300971));
#31372=CARTESIAN_POINT('Ctrl Pts',(0.106838781720774,-0.149605051766532,
0.700003398058251));
#31373=CARTESIAN_POINT('Ctrl Pts',(0.183637062036826,0.00858057341481814,
0.711114563106797));
#31374=CARTESIAN_POINT('Ctrl Pts',(0.0924229284360449,0.1589156980696,0.722225728155339));
#31375=CARTESIAN_POINT('Ctrl Pts',(-0.0833503847528551,0.163856370505402,
0.733336893203883));
#31376=CARTESIAN_POINT('Ctrl Pts',(-0.182865130156443,0.0188822924059537,
0.744448058252428));
#31377=CARTESIAN_POINT('Ctrl Pts',(-0.115073714167466,-0.143367489694622,
0.75555922330097));
#31378=CARTESIAN_POINT('Ctrl Pts',(0.0580004387659595,-0.174448118065669,
0.766670388349515));
#31379=CARTESIAN_POINT('Ctrl Pts',(0.17800908511122,-0.0459234407622611,
0.777781553398057));
#31380=CARTESIAN_POINT('Ctrl Pts',(0.135154441460109,0.124617309179735,
0.788892718446602));
#31381=CARTESIAN_POINT('Ctrl Pts',(-0.0313551099181417,0.181143738163968,
0.800003883495145));
#31382=CARTESIAN_POINT('Ctrl Pts',(-0.169177381899564,0.0719389341505889,
0.81111504854369));
#31383=CARTESIAN_POINT('Ctrl Pts',(-0.152216626984007,-0.103083923397808,
0.822226213592232));
#31384=CARTESIAN_POINT('Ctrl Pts',(0.00400949547363229,-0.183793690702293,
0.833337378640777));
#31385=CARTESIAN_POINT('Ctrl Pts',(0.156567267939011,-0.0963477420579929,
0.844448543689319));
#31386=CARTESIAN_POINT('Ctrl Pts',(0.165879203582308,0.0792482593671729,
0.855559708737864));
#31387=CARTESIAN_POINT('Ctrl Pts',(0.0234256671005791,0.182338791618694,
0.866670873786407));
#31388=CARTESIAN_POINT('Ctrl Pts',(-0.140460377720211,0.118604717671243,
0.877782038834952));
#31389=CARTESIAN_POINT('Ctrl Pts',(-0.175837031067501,-0.0536426631484242,
0.888893203883495));
#31390=CARTESIAN_POINT('Ctrl Pts',(-0.0503376402892206,-0.17681153483915,
0.900004368932038));
#31391=CARTESIAN_POINT('Ctrl Pts',(0.12121644264892,-0.138212772940753,
0.911115533980582));
#31392=CARTESIAN_POINT('Ctrl Pts',(0.181867711471885,0.026839009932345,
0.922226699029127));
#31393=CARTESIAN_POINT('Ctrl Pts',(0.0761253709552246,0.167335367481701,
0.933337864077668));
#31394=CARTESIAN_POINT('Ctrl Pts',(-0.099265255914171,0.154733978795034,
0.944449029126215));
#31395=CARTESIAN_POINT('Ctrl Pts',(-0.18383655777075,0.000564071579882353,
0.955560194174756));
#31396=CARTESIAN_POINT('Ctrl Pts',(-0.100212911067809,-0.154121939161292,
0.966671359223301));
#31397=CARTESIAN_POINT('Ctrl Pts',(0.0750970673805211,-0.167799333720618,
0.977782524271844));
#31398=CARTESIAN_POINT('Ctrl Pts',(0.181699613594968,-0.0279545920640164,
0.988893689320389));
#31399=CARTESIAN_POINT('Ctrl Pts',(0.122062258834496,0.137466418983892,
1.00000485436893));
#31400=CARTESIAN_POINT('Ctrl Pts',(-0.0492515922639386,0.177116921324136,
1.01111601941748));
#31401=CARTESIAN_POINT('Ctrl Pts',(-0.175504715049764,0.0547210291375423,
1.02222718446602));
#31402=CARTESIAN_POINT('Ctrl Pts',(-0.14118522196555,-0.1177412066494,1.03333834951456));
#31403=CARTESIAN_POINT('Ctrl Pts',(0.0223056668548975,-0.182477852394609,
1.04444951456311));
#31404=CARTESIAN_POINT('Ctrl Pts',(0.165390974917898,-0.0802670846854376,
1.05556067961165));
#31405=CARTESIAN_POINT('Ctrl Pts',(0.157153269033781,0.0953897085409752,
1.06667184466019));
#31406=CARTESIAN_POINT('Ctrl Pts',(0.00514163720288116,0.183756944970195,
1.07778300970874));
#31407=CARTESIAN_POINT('Ctrl Pts',(-0.151589489028199,0.104032592396117,
1.08889417475728));
#31408=CARTESIAN_POINT('Ctrl Pts',(-0.169599832986023,-0.0709309104380943,
1.10000533980583));
#31409=CARTESIAN_POINT('Ctrl Pts',(-0.0324962964057439,-0.180887727526569,
1.11111650485437));
#31410=CARTESIAN_POINT('Ctrl Pts',(0.134445241673909,-0.125560970886474,
1.12222766990291));
#31411=CARTESIAN_POINT('Ctrl Pts',(0.178171768593789,0.0450698535437549,
1.13333883495146));
#31412=CARTESIAN_POINT('Ctrl Pts',(0.0989503531151977,0.130685679928735,
1.14074627831715));
#31413=CARTESIAN_POINT('Ctrl Pts',(0.0499806597877626,0.147301514408983,
1.14445));
#31414=CARTESIAN_POINT('',(0.0903606778650206,-0.126612599672284,0.));
#31415=CARTESIAN_POINT('Ctrl Pts',(0.0903606778650208,-0.126612599672284,
-2.77555756156289E-16));
#31416=CARTESIAN_POINT('Ctrl Pts',(0.132452439122316,-0.0965726187415828,
0.00370372168284762));
#31417=CARTESIAN_POINT('Ctrl Pts',(0.183597970935092,0.00826171234133487,
0.0111111650485434));
#31418=CARTESIAN_POINT('Ctrl Pts',(0.0924933321163406,0.159015923519395,
0.0222223300970871));
#31419=CARTESIAN_POINT('Ctrl Pts',(-0.0833119343177651,0.163815447531815,
0.0333334951456308));
#31420=CARTESIAN_POINT('Ctrl Pts',(-0.15310616378989,0.0622578531632503,
0.0411241775931451));
#31421=CARTESIAN_POINT('Ctrl Pts',(-0.155772922446558,0.00543356393242454,
0.0452111383578116));
#31422=CARTESIAN_POINT('Ctrl Pts',(-0.155735926886437,0.000101346774827265,
0.0455943774396301));
#31423=CARTESIAN_POINT('Ctrl Pts',(0.0863567639152676,0.175641488315944,
2.2659825404947E-17));
#31424=CARTESIAN_POINT('Ctrl Pts',(0.0902605506355985,0.173244147111074,
2.45989142876686E-17));
#31425=CARTESIAN_POINT('Ctrl Pts',(0.0940681517855526,0.170703362163956,
1.50959816364938E-17));
#31426=CARTESIAN_POINT('Ctrl Pts',(0.0977705169885396,0.168018661523996,
1.10588621593521E-17));
#31427=CARTESIAN_POINT('Ctrl Pts',(0.104919852250204,0.162834455239647,
2.72100915479622E-18));
#31428=CARTESIAN_POINT('Ctrl Pts',(0.111677400716997,0.157113958337607,
-2.16691070983975E-17));
#31429=CARTESIAN_POINT('Ctrl Pts',(0.118012246833275,0.150919901422416,
-3.33934269125535E-17));
#31430=CARTESIAN_POINT('Ctrl Pts',(0.122832506482077,0.146206769948873,
-4.2314601108814E-17));
#31431=CARTESIAN_POINT('Ctrl Pts',(0.127411584310215,0.141213843322959,
-4.34283416288416E-17));
#31432=CARTESIAN_POINT('Ctrl Pts',(0.131710542479305,0.135995360136636,
-4.0766001685455E-17));
#31433=CARTESIAN_POINT('Ctrl Pts',(0.136227531634889,0.130512210258439,
-3.79686353981478E-17));
#31434=CARTESIAN_POINT('Ctrl Pts',(0.140440157604184,0.124776412163605,
1.15313389293564E-17));
#31435=CARTESIAN_POINT('Ctrl Pts',(0.144331170139148,0.11882042578862,3.72965547335014E-17));
#31436=CARTESIAN_POINT('Ctrl Pts',(0.147802837134673,0.113506333084464,
6.02849796064744E-17));
#31437=CARTESIAN_POINT('Ctrl Pts',(0.15101843405387,0.108016870008689,-1.53625880027527E-18));
#31438=CARTESIAN_POINT('Ctrl Pts',(0.153962315598392,0.102374391558266,
-8.67361737988404E-18));
#31439=CARTESIAN_POINT('Ctrl Pts',(0.15571005357274,0.0990245373918854,
-1.29109592829026E-17));
#31440=CARTESIAN_POINT('Ctrl Pts',(0.157357576324963,0.0956291376942575,
-3.44593994380303E-18));
#31441=CARTESIAN_POINT('Ctrl Pts',(0.158902506880511,0.0921936740973187,
-6.07153216591882E-18));
#31442=CARTESIAN_POINT('Ctrl Pts',(0.163908283820673,0.0810623229886477,
-1.45787941606636E-17));
#31443=CARTESIAN_POINT('Ctrl Pts',(0.167841697827597,0.0695089356622268,
-9.75260753403157E-18));
#31444=CARTESIAN_POINT('Ctrl Pts',(0.170598119604662,0.0576980955231356,
-5.20417042793042E-18));
#31445=CARTESIAN_POINT('Ctrl Pts',(0.171984491688748,0.0517577059954232,
-2.91648489207139E-18));
#31446=CARTESIAN_POINT('Ctrl Pts',(0.173072324320188,0.0457521241966622,
1.08654590748341E-17));
#31447=CARTESIAN_POINT('Ctrl Pts',(0.173843127025583,0.0397030009933723,
1.73472347597681E-17));
#31448=CARTESIAN_POINT('Ctrl Pts',(0.174324086814962,0.0359285136940646,
2.13916853648473E-17));
#31449=CARTESIAN_POINT('Ctrl Pts',(0.17468129632341,0.0321360477424029,
-3.73379012875618E-17));
#31450=CARTESIAN_POINT('Ctrl Pts',(0.174909438673913,0.0283479136595781,
-3.46944695195361E-17));
#31451=CARTESIAN_POINT('Ctrl Pts',(0.175317247780942,0.0215765466853118,
-2.99692812919358E-17));
#31452=CARTESIAN_POINT('Ctrl Pts',(0.175315000224248,0.0148063200599795,
-5.50593613673983E-17));
#31453=CARTESIAN_POINT('Ctrl Pts',(0.174882170147482,0.00806701752180915,
-4.68375338513738E-17));
#31454=CARTESIAN_POINT('Ctrl Pts',(0.174454769721774,0.00141225638482493,
-4.0453568795602E-17));
#31455=CARTESIAN_POINT('Ctrl Pts',(0.173607423807277,-0.00521244743448051,
5.53912001912299E-18));
#31456=CARTESIAN_POINT('Ctrl Pts',(0.172357876958299,-0.0117762500451153,
6.93889390390723E-18));
#31457=CARTESIAN_POINT('Ctrl Pts',(0.171266545977134,-0.0175089531839406,
8.16143038450564E-18));
#31458=CARTESIAN_POINT('Ctrl Pts',(0.169868307866471,-0.0231952127882146,
5.24172218001205E-19));
#31459=CARTESIAN_POINT('Ctrl Pts',(0.168172344307035,-0.0288124942050995,
-3.46944695195361E-18));
#31460=CARTESIAN_POINT('Ctrl Pts',(0.167269600009596,-0.0318025164482014,
-5.59521015704244E-18));
#31461=CARTESIAN_POINT('Ctrl Pts',(0.166282932031305,-0.0347708579305845,
-1.1797187803688E-17));
#31462=CARTESIAN_POINT('Ctrl Pts',(0.165217237950495,-0.0377059593473793,
-8.67361737988404E-18));
#31463=CARTESIAN_POINT('Ctrl Pts',(0.161836480623691,-0.047017135789496,
1.23544919580411E-18));
#31464=CARTESIAN_POINT('Ctrl Pts',(0.157654897120342,-0.0560198074489911,
-1.7088045241211E-17));
#31465=CARTESIAN_POINT('Ctrl Pts',(0.152731837788828,-0.0646106508942882,
1.38777878078145E-17));
#31466=CARTESIAN_POINT('Ctrl Pts',(0.14995806869425,-0.0694509370741418,
3.13246770113308E-17));
#31467=CARTESIAN_POINT('Ctrl Pts',(0.146948492244732,-0.074160201986225,
-2.50126624213863E-18));
#31468=CARTESIAN_POINT('Ctrl Pts',(0.143711118647294,-0.0787168991005189,
3.46944695195361E-18));
#31469=CARTESIAN_POINT('Ctrl Pts',(0.141667380230334,-0.0815935201226661,
7.2387295398745E-18));
#31470=CARTESIAN_POINT('Ctrl Pts',(0.139532823645962,-0.0844092886780934,
1.73900611772481E-17));
#31471=CARTESIAN_POINT('Ctrl Pts',(0.137309196652862,-0.08715819230643,
2.08166817117217E-17));
#31472=CARTESIAN_POINT('Ctrl Pts',(0.135173374337891,-0.0897985495827733,
2.41079947894884E-17));
#31473=CARTESIAN_POINT('Ctrl Pts',(0.132961417486925,-0.0923697150592745,
-3.29131307776674E-18));
#31474=CARTESIAN_POINT('Ctrl Pts',(0.130676581353388,-0.0948665968574491,
0.));
#31475=CARTESIAN_POINT('Ctrl Pts',(0.123427275316167,-0.10278867933332,
1.04426463739872E-17));
#31476=CARTESIAN_POINT('Ctrl Pts',(0.115443266551879,-0.109969536302748,
2.37276977285196E-17));
#31477=CARTESIAN_POINT('Ctrl Pts',(0.106786977446893,-0.116251471062968,
2.77555756156289E-17));
#31478=CARTESIAN_POINT('Ctrl Pts',(0.101553949468808,-0.120049119218897,
3.01905679570255E-17));
#31479=CARTESIAN_POINT('Ctrl Pts',(0.0960747579407472,-0.123517461158967,
2.18989005301202E-17));
#31480=CARTESIAN_POINT('Ctrl Pts',(0.0903606778650241,-0.126612599672281,
2.08166817117217E-17));
#31481=CARTESIAN_POINT('Ctrl Pts',(0.188079991776263,-0.0516378774142081,
1.1046));
#31482=CARTESIAN_POINT('Ctrl Pts',(0.179754570390634,-0.0821182550519846,
1.1028067538919));
#31483=CARTESIAN_POINT('Ctrl Pts',(0.164446793279769,-0.110682480125595,
1.1010135077838));
#31484=CARTESIAN_POINT('Ctrl Pts',(0.143091597726206,-0.133587557506818,
1.09922026167571));
#31485=CARTESIAN_POINT('Ctrl Pts',(0.0989851583166799,-0.180895080641009,
1.09551653999286));
#31486=CARTESIAN_POINT('Ctrl Pts',(0.0290818548970629,-0.204062011418838,
1.09181281831001));
#31487=CARTESIAN_POINT('Ctrl Pts',(-0.0345744266721549,-0.19262440956347,
1.08810909662716));
#31488=CARTESIAN_POINT('Ctrl Pts',(-0.0982307082413709,-0.181186807708102,
1.08440537494431));
#31489=CARTESIAN_POINT('Ctrl Pts',(-0.155639967960188,-0.135144673219537,
1.08070165326147));
#31490=CARTESIAN_POINT('Ctrl Pts',(-0.180573868997825,-0.0754924386616321,
1.07699793157862));
#31491=CARTESIAN_POINT('Ctrl Pts',(-0.190472245868201,-0.0518114150655666,
1.07552761078989));
#31492=CARTESIAN_POINT('Ctrl Pts',(-0.195252608806662,-0.0259854826956367,
1.07405729000116));
#31493=CARTESIAN_POINT('Ctrl Pts',(-0.195129684289216,-0.000113636086278679,
1.07258696921242));
#31494=CARTESIAN_POINT('Origin',(0.,0.,-0.129405622560369));
#31495=CARTESIAN_POINT('',(-0.0903606778650173,-0.126612599672286,0.));
#31496=CARTESIAN_POINT('Ctrl Pts',(-0.0905549614304886,-0.126792015305981,
1.24276674021151E-16));
#31497=CARTESIAN_POINT('Ctrl Pts',(-0.0513706458239086,-0.154472437079514,
0.00344950590738082));
#31498=CARTESIAN_POINT('Ctrl Pts',(0.0587535178885047,-0.172169358136003,
0.0106052258091336));
#31499=CARTESIAN_POINT('Ctrl Pts',(0.177508460417327,-0.0479721809770191,
0.0214671597052585));
#31500=CARTESIAN_POINT('Ctrl Pts',(0.13650560094313,0.123222299189869,0.0325858016883748));
#31501=CARTESIAN_POINT('Ctrl Pts',(-0.0295638381403906,0.181478253869214,
0.043704443671491));
#31502=CARTESIAN_POINT('Ctrl Pts',(-0.141307745535963,0.0946781319192958,
0.0526443839621562));
#31503=CARTESIAN_POINT('Ctrl Pts',(-0.155414936746312,0.0214718667413076,
0.0578781102584494));
#31504=CARTESIAN_POINT('Ctrl Pts',(-0.155326046963413,7.29270061605551E-5,
0.0594056225603705));
#31505=CARTESIAN_POINT('Origin',(0.,0.,0.));
#31506=CARTESIAN_POINT('Ctrl Pts',(-0.0685825729128748,0.139614588036674,
-0.0230074082272066));
#31507=CARTESIAN_POINT('Ctrl Pts',(-0.115028016933624,0.116799292759742,
-0.0193011942328345));
#31508=CARTESIAN_POINT('Ctrl Pts',(-0.182555218707277,0.0215691441263552,
-0.0118887662440903));
#31509=CARTESIAN_POINT('Ctrl Pts',(-0.116942936218886,-0.142059634545264,
-0.000770124260974049));
#31510=CARTESIAN_POINT('Ctrl Pts',(0.0559468948314244,-0.175104601534012,
0.0103485177221422));
#31511=CARTESIAN_POINT('Ctrl Pts',(0.177508460417327,-0.0479721809770191,
0.0214671597052585));
#31512=CARTESIAN_POINT('Ctrl Pts',(0.13650560094313,0.123222299189869,0.0325858016883748));
#31513=CARTESIAN_POINT('Ctrl Pts',(-0.0295638381403906,0.181478253869214,
0.043704443671491));
#31514=CARTESIAN_POINT('Ctrl Pts',(-0.168540213790592,0.0735245708832444,
0.0548230856546073));
#31515=CARTESIAN_POINT('Ctrl Pts',(-0.153132379752993,-0.101797781965797,
0.0659417276377235));
#31516=CARTESIAN_POINT('Ctrl Pts',(0.00255447675030308,-0.183860034663711,
0.0770603696208398));
#31517=CARTESIAN_POINT('Ctrl Pts',(0.155899683301632,-0.0975032021788082,
0.0881790116039561));
#31518=CARTESIAN_POINT('Ctrl Pts',(0.166434877052597,0.0781732535368643,
0.0992976535870723));
#31519=CARTESIAN_POINT('Ctrl Pts',(0.0245080507541896,0.182238325373942,
0.110416295570189));
#31520=CARTESIAN_POINT('Ctrl Pts',(-0.139868975820189,0.119365863723167,
0.121534937553305));
#31521=CARTESIAN_POINT('Ctrl Pts',(-0.176120077222934,-0.0528512641939849,
0.132653579536421));
#31522=CARTESIAN_POINT('Ctrl Pts',(-0.0510374815939226,-0.176654153931159,
0.143772221519537));
#31523=CARTESIAN_POINT('Ctrl Pts',(0.120797626960931,-0.138634273102519,
0.154890863502654));
#31524=CARTESIAN_POINT('Ctrl Pts',(0.181976886629041,0.0263806680570579,
0.16600950548577));
#31525=CARTESIAN_POINT('Ctrl Pts',(0.0764574137846417,0.167229745635935,
0.177128147468886));
#31526=CARTESIAN_POINT('Ctrl Pts',(-0.0991003621173195,0.154889135395602,
0.188246789452002));
#31527=CARTESIAN_POINT('Ctrl Pts',(-0.183877909581896,0.000663349951290586,
0.199365431435119));
#31528=CARTESIAN_POINT('Ctrl Pts',(-0.100215313155719,-0.154170088892816,
0.210484073418235));
#31529=CARTESIAN_POINT('Ctrl Pts',(0.0752488571272716,-0.167777039880966,
0.221602715401351));
#31530=CARTESIAN_POINT('Ctrl Pts',(0.181781810074028,-0.0276929424335053,
0.232721357384467));
#31531=CARTESIAN_POINT('Ctrl Pts',(0.121794738393109,0.137759091140133,
0.243839999367584));
#31532=CARTESIAN_POINT('Ctrl Pts',(-0.0497615974795104,0.177017821004958,
0.2549586413507));
#31533=CARTESIAN_POINT('Ctrl Pts',(-0.175734151264734,0.0541205469518692,
0.266077283333817));
#31534=CARTESIAN_POINT('Ctrl Pts',(-0.140726598433086,-0.11835349598584,
0.277195925316932));
#31535=CARTESIAN_POINT('Ctrl Pts',(0.0231926238140432,-0.182410602009977,
0.288314567300049));
#31536=CARTESIAN_POINT('Ctrl Pts',(0.165866396469461,-0.0793716828903688,
0.299433209283165));
#31537=CARTESIAN_POINT('Ctrl Pts',(0.156599354026699,0.096375141196464,
0.310551851266282));
#31538=CARTESIAN_POINT('Ctrl Pts',(0.00388050940998321,0.183838154825996,
0.321670493249398));
#31539=CARTESIAN_POINT('Ctrl Pts',(-0.152393050178991,0.102897443019027,
0.332789135232514));
#31540=CARTESIAN_POINT('Ctrl Pts',(-0.169067964401488,-0.0723017906820314,
0.34390777721563));
#31541=CARTESIAN_POINT('Ctrl Pts',(-0.0308692884081366,-0.181269447386996,
0.355026419198746));
#31542=CARTESIAN_POINT('Ctrl Pts',(0.135606994996762,-0.124186426112907,
0.366145061181863));
#31543=CARTESIAN_POINT('Ctrl Pts',(0.177861387826841,0.0466567491694538,
0.377263703164979));
#31544=CARTESIAN_POINT('Ctrl Pts',(0.0571870330903418,0.174760318061885,
0.388382345148095));
#31545=CARTESIAN_POINT('Ctrl Pts',(-0.115873124952358,0.142775853828764,
0.399500987131212));
#31546=CARTESIAN_POINT('Ctrl Pts',(-0.182788473512851,-0.0199974866820836,
0.410619629114327));
#31547=CARTESIAN_POINT('Ctrl Pts',(-0.0822616502622442,-0.164452261823584,
0.421738271097444));
#31548=CARTESIAN_POINT('Ctrl Pts',(0.0936204134582059,-0.158261630557358,
0.43285691308056));
#31549=CARTESIAN_POINT('Ctrl Pts',(0.183742116834086,-0.00709647969689106,
0.443975555063676));
#31550=CARTESIAN_POINT('Ctrl Pts',(0.10554806974386,0.150569354438759,0.455094197046793));
#31551=CARTESIAN_POINT('Ctrl Pts',(-0.0693325883166112,0.170307127625589,
0.466212839029909));
#31552=CARTESIAN_POINT('Ctrl Pts',(-0.180701587562324,0.0340361833232659,
0.477331481013025));
#31553=CARTESIAN_POINT('Ctrl Pts',(-0.126540093064824,-0.133413381524886,
0.488450122996142));
#31554=CARTESIAN_POINT('Ctrl Pts',(0.0435376164803608,-0.17865050090601,
0.499568764979258));
#31555=CARTESIAN_POINT('Ctrl Pts',(0.173732980498774,-0.0602360109052031,
0.510687406962374));
#31556=CARTESIAN_POINT('Ctrl Pts',(0.144781397169404,0.113357278356683,
0.521806048945491));
#31557=CARTESIAN_POINT('Ctrl Pts',(-0.0167962271460079,0.183110382765203,
0.532924690928607));
#31558=CARTESIAN_POINT('Ctrl Pts',(-0.162987778710162,0.0851264325217889,
0.544043332911723));
#31559=CARTESIAN_POINT('Ctrl Pts',(-0.159875453933454,-0.0908370230265797,
0.555161974894839));
#31560=CARTESIAN_POINT('Ctrl Pts',(-0.0103102773360761,-0.183589824620028,
0.566280616877956));
#31561=CARTESIAN_POINT('Ctrl Pts',(0.14869956060099,-0.108166382022474,
0.577399258861071));
#31562=CARTESIAN_POINT('Ctrl Pts',(0.171494149863546,0.0663421591850832,
0.588517900844189));
#31563=CARTESIAN_POINT('Ctrl Pts',(0.0371926577693494,0.180078404398782,
0.599636542827304));
#31564=CARTESIAN_POINT('Ctrl Pts',(-0.1311789224034,0.128855018683177,0.610755184810421));
#31565=CARTESIAN_POINT('Ctrl Pts',(-0.179384918603911,-0.0404051543769803,
0.621873826793537));
#31566=CARTESIAN_POINT('Ctrl Pts',(-0.0632665469493242,-0.172652453095426,
0.632992468776653));
#31567=CARTESIAN_POINT('Ctrl Pts',(0.110806726459172,-0.146742614445027,
0.644111110759769));
#31568=CARTESIAN_POINT('Ctrl Pts',(0.183376231205259,0.0135898253011021,
0.655229752742886));
#31569=CARTESIAN_POINT('Ctrl Pts',(0.0879651525947856,0.161473395492061,
0.666348394726001));
#31570=CARTESIAN_POINT('Ctrl Pts',(-0.0880258220622017,0.161440330069759,
0.677467036709119));
#31571=CARTESIAN_POINT('Ctrl Pts',(-0.183381324808445,0.013520918395534,
0.688585678692234));
#31572=CARTESIAN_POINT('Ctrl Pts',(-0.11075157823663,-0.146784241118916,
0.699704320675351));
#31573=CARTESIAN_POINT('Ctrl Pts',(0.0633314188332071,-0.172628667698419,
0.710822962658467));
#31574=CARTESIAN_POINT('Ctrl Pts',(0.17940008868909,-0.0403377453646542,
0.721941604641583));
#31575=CARTESIAN_POINT('Ctrl Pts',(0.131130494233742,0.128904301731096,
0.733060246624699));
#31576=CARTESIAN_POINT('Ctrl Pts',(-0.0372603218894873,0.180064416072257,
0.744178888607816));
#31577=CARTESIAN_POINT('Ctrl Pts',(-0.171519066664489,0.0662777133981789,
0.755297530590932));
#31578=CARTESIAN_POINT('Ctrl Pts',(-0.148658905212271,-0.108222250133236,
0.766416172574049));
#31579=CARTESIAN_POINT('Ctrl Pts',(0.0103792628149562,-0.18358593744105,
0.777534814557165));
#31580=CARTESIAN_POINT('Ctrl Pts',(0.159909575810308,-0.0907769413831382,
0.78865345654028));
#31581=CARTESIAN_POINT('Ctrl Pts',(0.162955779866738,0.0851876712390422,
0.799772098523398));
#31582=CARTESIAN_POINT('Ctrl Pts',(0.0167274199086701,0.183116681231986,
0.810890740506512));
#31583=CARTESIAN_POINT('Ctrl Pts',(-0.144823982381472,0.11330286690894,
0.82200938248963));
#31584=CARTESIAN_POINT('Ctrl Pts',(-0.173710333792674,-0.0603012890298399,
0.833128024472746));
#31585=CARTESIAN_POINT('Ctrl Pts',(-0.0434704832044991,-0.178666848096071,
0.844246666455862));
#31586=CARTESIAN_POINT('Ctrl Pts',(0.126590215885116,-0.133365823077974,
0.855365308438979));
#31587=CARTESIAN_POINT('Ctrl Pts',(0.18068878531032,0.0341040818691465,
0.866483950422094));
#31588=CARTESIAN_POINT('Ctrl Pts',(0.069268588294083,0.170333168137465,
0.877602592405212));
#31589=CARTESIAN_POINT('Ctrl Pts',(-0.105604640517969,0.15052968290502,
0.888721234388326));
#31590=CARTESIAN_POINT('Ctrl Pts',(-0.183739437498563,-0.00716552286239433,
0.899839876371444));
#31591=CARTESIAN_POINT('Ctrl Pts',(-0.0935609375970031,-0.15829679799695,
0.91095851835456));
#31592=CARTESIAN_POINT('Ctrl Pts',(0.0823234386500799,-0.164421340203127,
0.922077160337675));
#31593=CARTESIAN_POINT('Ctrl Pts',(0.182795976495949,-0.0199287985657338,
0.933195802320793));
#31594=CARTESIAN_POINT('Ctrl Pts',(0.115819463928053,0.142819381470141,
0.944314444303908));
#31595=CARTESIAN_POINT('Ctrl Pts',(-0.0572526917402423,0.174738822826618,
0.955433086287024));
#31596=CARTESIAN_POINT('Ctrl Pts',(-0.177878918025408,0.046589901053406,
0.966551728270142));
#31597=CARTESIAN_POINT('Ctrl Pts',(-0.135560300066214,-0.124237352171324,
0.977670370253256));
#31598=CARTESIAN_POINT('Ctrl Pts',(0.0309373610575528,-0.181257875466721,
0.988789012236375));
#31599=CARTESIAN_POINT('Ctrl Pts',(0.169095195914933,-0.0722381792257861,
0.999907654219489));
#31600=CARTESIAN_POINT('Ctrl Pts',(0.152354231364944,0.102954552944809,
1.01102629620261));
#31601=CARTESIAN_POINT('Ctrl Pts',(-0.00394931635484403,0.183836962465064,
1.02214493818572));
#31602=CARTESIAN_POINT('Ctrl Pts',(-0.156636075542215,0.0963157594965877,
1.03326358016884));
#31603=CARTESIAN_POINT('Ctrl Pts',(-0.165835572967195,-0.0794329933758677,
1.04438222215196));
#31604=CARTESIAN_POINT('Ctrl Pts',(-0.0231259578302998,-0.182421227428175,
1.05550086413507));
#31605=CARTESIAN_POINT('Ctrl Pts',(0.140774638007895,-0.11829694620695,
1.06661950611819));
#31606=CARTESIAN_POINT('Ctrl Pts',(0.175706993010233,0.0541796064983141,
1.07773814810131));
#31607=CARTESIAN_POINT('Ctrl Pts',(0.0497080432048737,0.177049779856472,
1.08885679008442));
#31608=CARTESIAN_POINT('Ctrl Pts',(-0.121871201614337,0.137688031013954,
1.09997543206754));
#31609=CARTESIAN_POINT('Ctrl Pts',(-0.181724153253684,-0.027712968875509,
1.11109407405065));
#31610=CARTESIAN_POINT('Ctrl Pts',(-0.075277483453787,-0.167898453189698,
1.12221271603377));
#31611=CARTESIAN_POINT('Ctrl Pts',(0.100462758039806,-0.153944373403644,
1.13333135801688));
#31612=CARTESIAN_POINT('Ctrl Pts',(0.155754888396286,-0.0511266487217653,
1.14074378600563));
#31613=CARTESIAN_POINT('Ctrl Pts',(0.155548765964692,0.000619602180124784,
1.14445));
#31614=CARTESIAN_POINT('Ctrl Pts',(-0.074439243930934,0.151537102412034,
-0.0153382721514711));
#31615=CARTESIAN_POINT('Ctrl Pts',(-0.124850938769699,0.126773474301532,
-0.011632058157099));
#31616=CARTESIAN_POINT('Ctrl Pts',(-0.198144687185762,0.0234110607521693,
-0.0042196301683548));
#31617=CARTESIAN_POINT('Ctrl Pts',(-0.126929384324154,-0.154190945884872,
0.00689901181476148));
#31618=CARTESIAN_POINT('Ctrl Pts',(0.0607245306591998,-0.190057817801302,
0.0180176537978778));
#31619=CARTESIAN_POINT('Ctrl Pts',(0.192666956394248,-0.0520688088821623,
0.029136295780994));
#31620=CARTESIAN_POINT('Ctrl Pts',(0.148162620545796,0.133744979191402,
0.0402549377641103));
#31621=CARTESIAN_POINT('Ctrl Pts',(-0.0320884689126903,0.19697575395855,
0.0513735797472264));
#31622=CARTESIAN_POINT('Ctrl Pts',(-0.182932858212653,0.0798032683003624,
0.0624922217303428));
#31623=CARTESIAN_POINT('Ctrl Pts',(-0.166209258212561,-0.110490895887015,
0.0736108637134591));
#31624=CARTESIAN_POINT('Ctrl Pts',(0.00277261860929502,-0.199560929084259,
0.0847295056965753));
#31625=CARTESIAN_POINT('Ctrl Pts',(0.169212878157669,-0.10582957656395,
0.0958481476796916));
#31626=CARTESIAN_POINT('Ctrl Pts',(0.180647734334385,0.0848489294255244,
0.106966789662808));
#31627=CARTESIAN_POINT('Ctrl Pts',(0.0266009379770665,0.197800732458805,
0.118085431645924));
#31628=CARTESIAN_POINT('Ctrl Pts',(-0.151813213871049,0.12955921992025,
0.129204073629041));
#31629=CARTESIAN_POINT('Ctrl Pts',(-0.191160010957712,-0.0573645458357494,
0.140322715612156));
#31630=CARTESIAN_POINT('Ctrl Pts',(-0.0553958736254638,-0.191739695630841,
0.151441357595273));
#31631=CARTESIAN_POINT('Ctrl Pts',(0.131113249878304,-0.150473072594935,
0.162559999578389));
#31632=CARTESIAN_POINT('Ctrl Pts',(0.19751696791516,0.0286334691329668,
0.173678641561505));
#31633=CARTESIAN_POINT('Ctrl Pts',(0.0829865639814035,0.181510481441338,
0.184797283544622));
#31634=CARTESIAN_POINT('Ctrl Pts',(-0.107563127424026,0.168116033596642,
0.195915925527738));
#31635=CARTESIAN_POINT('Ctrl Pts',(-0.199580330447296,0.000719997322039096,
0.207034567510854));
#31636=CARTESIAN_POINT('Ctrl Pts',(-0.108773290717609,-0.167335583465575,
0.218153209493971));
#31637=CARTESIAN_POINT('Ctrl Pts',(0.0816748015321165,-0.182104512374819,
0.229271851477087));
#31638=CARTESIAN_POINT('Ctrl Pts',(0.197305232620797,-0.0300578063700233,
0.240390493460203));
#31639=CARTESIAN_POINT('Ctrl Pts',(0.132195510545613,0.149523153675082,
0.251509135443319));
#31640=CARTESIAN_POINT('Ctrl Pts',(-0.054011034229875,0.192134418384253,
0.262627777426435));
#31641=CARTESIAN_POINT('Ctrl Pts',(-0.190741128502276,0.0587422201459823,
0.273746419409552));
#31642=CARTESIAN_POINT('Ctrl Pts',(-0.152744073944838,-0.128460400121777,
0.284865061392668));
#31643=CARTESIAN_POINT('Ctrl Pts',(0.0251731789602741,-0.19798772081443,
0.295983703375785));
#31644=CARTESIAN_POINT('Ctrl Pts',(0.180030707836241,-0.0861496997406464,
0.3071023453589));
#31645=CARTESIAN_POINT('Ctrl Pts',(0.169972297898904,0.104605183790867,
0.318220987342017));
#31646=CARTESIAN_POINT('Ctrl Pts',(0.00421188903066005,0.199537180797957,
0.329339629325133));
#31647=CARTESIAN_POINT('Ctrl Pts',(-0.165406792919015,0.111684463493277,
0.34045827130825));
#31648=CARTESIAN_POINT('Ctrl Pts',(-0.183505676565636,-0.0784760676748057,
0.351576913291366));
#31649=CARTESIAN_POINT('Ctrl Pts',(-0.0335053992900935,-0.196749116257395,
0.362695555274482));
#31650=CARTESIAN_POINT('Ctrl Pts',(0.147187277329603,-0.134791438607496,
0.373814197257599));
#31651=CARTESIAN_POINT('Ctrl Pts',(0.193050022360002,0.0506410445822938,
0.384932839240714));
#31652=CARTESIAN_POINT('Ctrl Pts',(0.0620705716495424,0.189684133929807,
0.396051481223831));
#31653=CARTESIAN_POINT('Ctrl Pts',(-0.125768215554202,0.154968327363698,
0.407170123206947));
#31654=CARTESIAN_POINT('Ctrl Pts',(-0.19839786099702,-0.0217051901949521,
0.418288765190064));
#31655=CARTESIAN_POINT('Ctrl Pts',(-0.0892864584974339,-0.178495811879663,
0.429407407173179));
#31656=CARTESIAN_POINT('Ctrl Pts',(0.101615213578872,-0.171776526041577,
0.440526049156296));
#31657=CARTESIAN_POINT('Ctrl Pts',(0.199432941554622,-0.00770249001709277,
0.451644691139412));
#31658=CARTESIAN_POINT('Ctrl Pts',(0.114561442891388,0.16342736102696,0.462763333122529));
#31659=CARTESIAN_POINT('Ctrl Pts',(-0.0752533075803338,0.184850659257176,
0.473881975105645));
#31660=CARTESIAN_POINT('Ctrl Pts',(-0.196132763527948,0.0369427340688636,
0.485000617088761));
#31661=CARTESIAN_POINT('Ctrl Pts',(-0.13734609908354,-0.144806338245697,
0.496119259071877));
#31662=CARTESIAN_POINT('Ctrl Pts',(0.0472555507281729,-0.19390652246629,
0.507237901054994));
#31663=CARTESIAN_POINT('Ctrl Pts',(0.188569065943703,-0.0653799196903168,
0.51835654303811));
#31664=CARTESIAN_POINT('Ctrl Pts',(0.157145135896933,0.123037525956625,
0.529475185021226));
#31665=CARTESIAN_POINT('Ctrl Pts',(-0.0182305561972616,0.198747259981946,
0.540593827004342));
#31666=CARTESIAN_POINT('Ctrl Pts',(-0.176906267902489,0.0923958814363803,
0.551712468987459));
#31667=CARTESIAN_POINT('Ctrl Pts',(-0.173528163328608,-0.0985941329968107,
0.562831110970574));
#31668=CARTESIAN_POINT('Ctrl Pts',(-0.0111907328205795,-0.199267644208816,
0.573949752953692));
#31669=CARTESIAN_POINT('Ctrl Pts',(0.161397894448518,-0.117403348321834,
0.585068394936807));
#31670=CARTESIAN_POINT('Ctrl Pts',(0.186139048335769,0.0720075080408093,
0.596187036919923));
#31671=CARTESIAN_POINT('Ctrl Pts',(0.0403687585131819,0.19545636307293,
0.60730567890304));
#31672=CARTESIAN_POINT('Ctrl Pts',(-0.142381065460884,0.139858709874703,
0.618424320886156));
#31673=CARTESIAN_POINT('Ctrl Pts',(-0.194703656429618,-0.0438555891823412,
0.629542962869273));
#31674=CARTESIAN_POINT('Ctrl Pts',(-0.0686692511086116,-0.187396265922711,
0.640661604852388));
#31675=CARTESIAN_POINT('Ctrl Pts',(0.120269167366484,-0.159273833100625,
0.651780246835506));
#31676=CARTESIAN_POINT('Ctrl Pts',(0.199035810790665,0.0147503407586138,
0.662898888818621));
#31677=CARTESIAN_POINT('Ctrl Pts',(0.0954770165847204,0.175262562555938,
0.674017530801738));
#31678=CARTESIAN_POINT('Ctrl Pts',(-0.09554286697633,0.17522667348191,0.685136172784854));
#31679=CARTESIAN_POINT('Ctrl Pts',(-0.199041339366714,0.0146755494853507,
0.69625481476797));
#31680=CARTESIAN_POINT('Ctrl Pts',(-0.120209309711463,-0.159319014522084,
0.707373456751086));
#31681=CARTESIAN_POINT('Ctrl Pts',(0.0687396627858533,-0.187370449350155,
0.718492098734203));
#31682=CARTESIAN_POINT('Ctrl Pts',(0.194720121977979,-0.0437824237162718,
0.729610740717318));
#31683=CARTESIAN_POINT('Ctrl Pts',(0.142328501723757,0.139912201493195,
0.740729382700435));
#31684=CARTESIAN_POINT('Ctrl Pts',(-0.0404422008722263,0.195441180200575,
0.751848024683551));
#31685=CARTESIAN_POINT('Ctrl Pts',(-0.186166092929526,0.0719375588474842,
0.762966666666667));
#31686=CARTESIAN_POINT('Ctrl Pts',(-0.161353767256008,-0.117463987340584,
0.774085308649784));
#31687=CARTESIAN_POINT('Ctrl Pts',(0.0112656093769942,-0.199263425080664,
0.7852039506329));
#31688=CARTESIAN_POINT('Ctrl Pts',(0.173565199074082,-0.0985289206269375,
0.796322592616017));
#31689=CARTESIAN_POINT('Ctrl Pts',(0.176871536488809,0.0924623496894334,
0.807441234599133));
#31690=CARTESIAN_POINT('Ctrl Pts',(0.0181558731034875,0.198754096312013,
0.818559876582249));
#31691=CARTESIAN_POINT('Ctrl Pts',(-0.157191357711808,0.122978467993954,
0.829678518565365));
#31692=CARTESIAN_POINT('Ctrl Pts',(-0.188544485301595,-0.06545077229961,
0.840797160548482));
#31693=CARTESIAN_POINT('Ctrl Pts',(-0.0471826845453332,-0.193924265639472,
0.851915802531597));
#31694=CARTESIAN_POINT('Ctrl Pts',(0.137400502187529,-0.144754718502077,
0.863034444514714));
#31695=CARTESIAN_POINT('Ctrl Pts',(0.196118868016023,0.0370164308726493,
0.87415308649783));
#31696=CARTESIAN_POINT('Ctrl Pts',(0.0751838422178375,0.184878923522181,
0.885271728480947));
#31697=CARTESIAN_POINT('Ctrl Pts',(-0.114622844578058,0.163384301706618,
0.896390370464062));
#31698=CARTESIAN_POINT('Ctrl Pts',(-0.199430033414812,-0.0077774291863319,
0.90750901244718));
#31699=CARTESIAN_POINT('Ctrl Pts',(-0.101550658722561,-0.171814696636568,
0.918627654430294));
#31700=CARTESIAN_POINT('Ctrl Pts',(0.0893535233606871,-0.178462249679383,
0.929746296413413));
#31701=CARTESIAN_POINT('Ctrl Pts',(0.198406004704164,-0.0216306363946107,
0.940864938396527));
#31702=CARTESIAN_POINT('Ctrl Pts',(0.12570997209806,0.155015572087487,0.951983580379645));
#31703=CARTESIAN_POINT('Ctrl Pts',(-0.0621418372793996,0.18966080308943,
0.963102222362759));
#31704=CARTESIAN_POINT('Ctrl Pts',(-0.193069049565776,0.050568487910749,
0.974220864345877));
#31705=CARTESIAN_POINT('Ctrl Pts',(-0.147136594843111,-0.134846713542859,
0.985339506328992));
#31706=CARTESIAN_POINT('Ctrl Pts',(0.0335792850651442,-0.196736556142493,
0.99645814831211));
#31707=CARTESIAN_POINT('Ctrl Pts',(0.183535233538869,-0.0784070240605622,
1.00757679029522));
#31708=CARTESIAN_POINT('Ctrl Pts',(0.165364659137136,0.111746450372967,
1.01869543227834));
#31709=CARTESIAN_POINT('Ctrl Pts',(-0.00428657180698079,0.199535886614283,
1.02981407426146));
#31710=CARTESIAN_POINT('Ctrl Pts',(-0.170012155281541,0.104540731136874,
1.04093271624457));
#31711=CARTESIAN_POINT('Ctrl Pts',(-0.179997252133044,-0.0862162458906591,
1.05205135822769));
#31712=CARTESIAN_POINT('Ctrl Pts',(-0.0251008199743871,-0.197999253599851,
1.06317000021081));
#31713=CARTESIAN_POINT('Ctrl Pts',(0.152796215902707,-0.128399021223231,
1.07428864219392));
#31714=CARTESIAN_POINT('Ctrl Pts',(0.190711651044001,0.0588063231359589,
1.08540728417704));
#31715=CARTESIAN_POINT('Ctrl Pts',(0.0539529066393858,0.192169106390877,
1.09652592616015));
#31716=CARTESIAN_POINT('Ctrl Pts',(-0.132278503412967,0.149446025304978,
1.10764456814327));
#31717=CARTESIAN_POINT('Ctrl Pts',(-0.197242652143987,-0.0300795429882017,
1.11876321012639));
#31718=CARTESIAN_POINT('Ctrl Pts',(-0.0817058724297523,-0.182236293883171,
1.12988185210951));
#31719=CARTESIAN_POINT('Ctrl Pts',(0.109041866382002,-0.167090592797485,
1.14100049409262));
#31720=CARTESIAN_POINT('Ctrl Pts',(0.169055718360052,-0.0554926552610627,
1.14841292208137));
#31721=CARTESIAN_POINT('Ctrl Pts',(0.16883199391646,0.000672513670271936,
1.15211913607574));
#31722=CARTESIAN_POINT('Ctrl Pts',(-0.0802959149489932,0.163459616787394,
-0.00766913607573554));
#31723=CARTESIAN_POINT('Ctrl Pts',(-0.134673860605774,0.136747655843322,
-0.00396292208136346));
#31724=CARTESIAN_POINT('Ctrl Pts',(-0.213734155664247,0.0252529773779836,
0.00344950590738073));
#31725=CARTESIAN_POINT('Ctrl Pts',(-0.136915832429422,-0.166322257224481,
0.014568147890497));
#31726=CARTESIAN_POINT('Ctrl Pts',(0.0655021664869751,-0.205011034068591,
0.0256867898736133));
#31727=CARTESIAN_POINT('Ctrl Pts',(0.20782545237117,-0.0561654367873057,
0.0368054318567295));
#31728=CARTESIAN_POINT('Ctrl Pts',(0.159819640148463,0.144267659192936,
0.0479240738398458));
#31729=CARTESIAN_POINT('Ctrl Pts',(-0.0346130996849898,0.212473254047885,
0.0590427158229621));
#31730=CARTESIAN_POINT('Ctrl Pts',(-0.197325502634714,0.0860819657174806,
0.0701613578060782));
#31731=CARTESIAN_POINT('Ctrl Pts',(-0.179286136672128,-0.119184009808233,
0.0812799997891947));
#31732=CARTESIAN_POINT('Ctrl Pts',(0.00299076046828686,-0.215261823504807,
0.0923986417723108));
#31733=CARTESIAN_POINT('Ctrl Pts',(0.182526073013706,-0.114155950949091,
0.103517283755427));
#31734=CARTESIAN_POINT('Ctrl Pts',(0.194860591616173,0.0915246053141843,
0.114635925738543));
#31735=CARTESIAN_POINT('Ctrl Pts',(0.0286938251999433,0.213363139543668,
0.12575456772166));
#31736=CARTESIAN_POINT('Ctrl Pts',(-0.163757451921909,0.139752576117334,
0.136873209704776));
#31737=CARTESIAN_POINT('Ctrl Pts',(-0.20619994469249,-0.0618778274775138,
0.147991851687892));
#31738=CARTESIAN_POINT('Ctrl Pts',(-0.0597542656570052,-0.206825237330522,
0.159110493671008));
#31739=CARTESIAN_POINT('Ctrl Pts',(0.141428872795678,-0.162311872087351,
0.170229135654125));
#31740=CARTESIAN_POINT('Ctrl Pts',(0.213057049201279,0.0308862702088754,
0.181347777637241));
#31741=CARTESIAN_POINT('Ctrl Pts',(0.0895157141781652,0.195791217246742,
0.192466419620357));
#31742=CARTESIAN_POINT('Ctrl Pts',(-0.116025892730732,0.181342931797682,
0.203585061603473));
#31743=CARTESIAN_POINT('Ctrl Pts',(-0.215282751312695,0.000776644692787891,
0.21470370358659));
#31744=CARTESIAN_POINT('Ctrl Pts',(-0.1173312682795,-0.180501078038335,
0.225822345569706));
#31745=CARTESIAN_POINT('Ctrl Pts',(0.0881007459369614,-0.196431984868673,
0.236940987552822));
#31746=CARTESIAN_POINT('Ctrl Pts',(0.212828655167567,-0.0324226703065412,
0.248059629535939));
#31747=CARTESIAN_POINT('Ctrl Pts',(0.142596282698117,0.16128721621003,0.259178271519055));
#31748=CARTESIAN_POINT('Ctrl Pts',(-0.0582604709802392,0.207251015763547,
0.270296913502171));
#31749=CARTESIAN_POINT('Ctrl Pts',(-0.205748105739819,0.0633638933400953,
0.281415555485287));
#31750=CARTESIAN_POINT('Ctrl Pts',(-0.16476154945659,-0.138567304257714,
0.292534197468403));
#31751=CARTESIAN_POINT('Ctrl Pts',(0.0271537341065049,-0.213564839618882,
0.30365283945152));
#31752=CARTESIAN_POINT('Ctrl Pts',(0.19419501920302,-0.092927716590924,
0.314771481434636));
#31753=CARTESIAN_POINT('Ctrl Pts',(0.183345241771109,0.11283522638527,0.325890123417753));
#31754=CARTESIAN_POINT('Ctrl Pts',(0.0045432686513366,0.215236206769919,
0.337008765400868));
#31755=CARTESIAN_POINT('Ctrl Pts',(-0.178420535659039,0.120471483967528,
0.348127407383985));
#31756=CARTESIAN_POINT('Ctrl Pts',(-0.197943388729784,-0.08465034466758,
0.359246049367101));
#31757=CARTESIAN_POINT('Ctrl Pts',(-0.0361415101720502,-0.212228785127794,
0.370364691350217));
#31758=CARTESIAN_POINT('Ctrl Pts',(0.158767559662444,-0.145396451102085,
0.381483333333334));
#31759=CARTESIAN_POINT('Ctrl Pts',(0.208238656893164,0.0546253399951339,
0.39260197531645));
#31760=CARTESIAN_POINT('Ctrl Pts',(0.0669541102087431,0.204607949797729,
0.403720617299566));
#31761=CARTESIAN_POINT('Ctrl Pts',(-0.135663306156047,0.167160800898631,
0.414839259282683));
#31762=CARTESIAN_POINT('Ctrl Pts',(-0.214007248481188,-0.0234128937078206,
0.425957901265799));
#31763=CARTESIAN_POINT('Ctrl Pts',(-0.0963112667326238,-0.192539361935742,
0.437076543248915));
#31764=CARTESIAN_POINT('Ctrl Pts',(0.109610013699538,-0.185291421525797,
0.448195185232032));
#31765=CARTESIAN_POINT('Ctrl Pts',(0.215123766275159,-0.00830850033729405,
0.459313827215147));
#31766=CARTESIAN_POINT('Ctrl Pts',(0.123574816038915,0.176285367615161,
0.470432469198265));
#31767=CARTESIAN_POINT('Ctrl Pts',(-0.0811740268440561,0.199394190888763,
0.48155111118138));
#31768=CARTESIAN_POINT('Ctrl Pts',(-0.211563939493572,0.0398492848144611,
0.492669753164497));
#31769=CARTESIAN_POINT('Ctrl Pts',(-0.148152105102257,-0.156199294966507,
0.503788395147612));
#31770=CARTESIAN_POINT('Ctrl Pts',(0.0509734849759847,-0.20916254402657,
0.51490703713073));
#31771=CARTESIAN_POINT('Ctrl Pts',(0.203405151388631,-0.0705238284754304,
0.526025679113844));
#31772=CARTESIAN_POINT('Ctrl Pts',(0.169508874624462,0.132717773556567,
0.537144321096963));
#31773=CARTESIAN_POINT('Ctrl Pts',(-0.019664885248515,0.21438413719869,
0.548262963080077));
#31774=CARTESIAN_POINT('Ctrl Pts',(-0.190824757094816,0.0996653303509719,
0.559381605063195));
#31775=CARTESIAN_POINT('Ctrl Pts',(-0.187180872723762,-0.106351242967042,
0.570500247046309));
#31776=CARTESIAN_POINT('Ctrl Pts',(-0.012071188305083,-0.214945463797604,
0.581618889029427));
#31777=CARTESIAN_POINT('Ctrl Pts',(0.174096228296046,-0.126640314621194,
0.592737531012542));
#31778=CARTESIAN_POINT('Ctrl Pts',(0.200783946807991,0.0776728568965356,
0.60385617299566));
#31779=CARTESIAN_POINT('Ctrl Pts',(0.0435448592570146,0.210834321747079,
0.614974814978775));
#31780=CARTESIAN_POINT('Ctrl Pts',(-0.153583208518367,0.150862401066228,
0.626093456961893));
#31781=CARTESIAN_POINT('Ctrl Pts',(-0.210022394255324,-0.0473060239877022,
0.637212098945007));
#31782=CARTESIAN_POINT('Ctrl Pts',(-0.074071955267899,-0.202140078749996,
0.648330740928124));
#31783=CARTESIAN_POINT('Ctrl Pts',(0.129731608273796,-0.171805051756223,
0.65944938291124));
#31784=CARTESIAN_POINT('Ctrl Pts',(0.214695390376071,0.015910856216126,
0.670568024894357));
#31785=CARTESIAN_POINT('Ctrl Pts',(0.102988880574655,0.189051729619815,
0.681686666877473));
#31786=CARTESIAN_POINT('Ctrl Pts',(-0.103059911890458,0.189013016894061,
0.692805308860589));
#31787=CARTESIAN_POINT('Ctrl Pts',(-0.214701353924984,0.0158301805751674,
0.703923950843705));
#31788=CARTESIAN_POINT('Ctrl Pts',(-0.129667041186295,-0.171853787925252,
0.715042592826822));
#31789=CARTESIAN_POINT('Ctrl Pts',(0.0741479067384996,-0.20211223100189,
0.726161234809938));
#31790=CARTESIAN_POINT('Ctrl Pts',(0.210040155266868,-0.0472271020678894,
0.737279876793055));
#31791=CARTESIAN_POINT('Ctrl Pts',(0.153526509213771,0.150920101255294,
0.748398518776171));
#31792=CARTESIAN_POINT('Ctrl Pts',(-0.0436240798549652,0.210817944328893,
0.759517160759286));
#31793=CARTESIAN_POINT('Ctrl Pts',(-0.200813119194563,0.0775974042967894,
0.770635802742404));
#31794=CARTESIAN_POINT('Ctrl Pts',(-0.174048629299744,-0.126705724547931,
0.781754444725519));
#31795=CARTESIAN_POINT('Ctrl Pts',(0.0121519559390324,-0.214940912720278,
0.792873086708636));
#31796=CARTESIAN_POINT('Ctrl Pts',(0.187220822337856,-0.106280899870737,
0.803991728691751));
#31797=CARTESIAN_POINT('Ctrl Pts',(0.190787293110882,0.0997370281398245,
0.815110370674869));
#31798=CARTESIAN_POINT('Ctrl Pts',(0.0195843262983046,0.21439151139204,
0.826229012657984));
#31799=CARTESIAN_POINT('Ctrl Pts',(-0.169558733042143,0.132654069078969,
0.837347654641101));
#31800=CARTESIAN_POINT('Ctrl Pts',(-0.203378636810517,-0.0706002555693802,
0.848466296624217));
#31801=CARTESIAN_POINT('Ctrl Pts',(-0.0508948858861673,-0.209181683182873,
0.859584938607333));
#31802=CARTESIAN_POINT('Ctrl Pts',(0.148210788489943,-0.156143613926181,
0.870703580590451));
#31803=CARTESIAN_POINT('Ctrl Pts',(0.211548950721726,0.0399287798761521,
0.881822222573564));
#31804=CARTESIAN_POINT('Ctrl Pts',(0.0810990961415922,0.199424678906897,
0.892940864556684));
#31805=CARTESIAN_POINT('Ctrl Pts',(-0.123641048638147,0.176238920508216,
0.904059506539796));
#31806=CARTESIAN_POINT('Ctrl Pts',(-0.215120629331062,-0.00838933551026959,
0.915178148522916));
#31807=CARTESIAN_POINT('Ctrl Pts',(-0.109540379848118,-0.185332595276186,
0.926296790506031));
#31808=CARTESIAN_POINT('Ctrl Pts',(0.0963836080712942,-0.19250315915564,
0.937415432489146));
#31809=CARTESIAN_POINT('Ctrl Pts',(0.214016032912378,-0.0233324742234878,
0.948534074472264));
#31810=CARTESIAN_POINT('Ctrl Pts',(0.135600480268067,0.167211762704833,
0.95965271645538));
#31811=CARTESIAN_POINT('Ctrl Pts',(-0.0670309828185569,0.204582783352242,
0.970771358438496));
#31812=CARTESIAN_POINT('Ctrl Pts',(-0.208259181106143,0.0545470747680921,
0.981890000421612));
#31813=CARTESIAN_POINT('Ctrl Pts',(-0.158712889620009,-0.145456074914393,
0.993008642404728));
#31814=CARTESIAN_POINT('Ctrl Pts',(0.0362212090727357,-0.212215236818265,
1.00412728438785));
#31815=CARTESIAN_POINT('Ctrl Pts',(0.197975271162805,-0.0845758688953388,
1.01524592637096));
#31816=CARTESIAN_POINT('Ctrl Pts',(0.178375086909329,0.120538347801125,
1.02636456835408));
#31817=CARTESIAN_POINT('Ctrl Pts',(-0.00462382725911752,0.215234810763501,
1.03748321033719));
#31818=CARTESIAN_POINT('Ctrl Pts',(-0.183388235020868,0.112765702777161,
1.04860185232031));
#31819=CARTESIAN_POINT('Ctrl Pts',(-0.194158931298892,-0.0929994984054507,
1.05972049430343));
#31820=CARTESIAN_POINT('Ctrl Pts',(-0.0270756821184746,-0.213577279771527,
1.07083913628654));
#31821=CARTESIAN_POINT('Ctrl Pts',(0.164817793797518,-0.138501096239512,
1.08195777826966));
#31822=CARTESIAN_POINT('Ctrl Pts',(0.20571630907777,0.0634330397736036,
1.09307642025277));
#31823=CARTESIAN_POINT('Ctrl Pts',(0.058197770073898,0.207288432925282,
1.10419506223589));
#31824=CARTESIAN_POINT('Ctrl Pts',(-0.142685805211597,0.161204019596003,
1.11531370421901));
#31825=CARTESIAN_POINT('Ctrl Pts',(-0.212761151034289,-0.0324461171008946,
1.12643234620212));
#31826=CARTESIAN_POINT('Ctrl Pts',(-0.0881342614057178,-0.196574134576644,
1.13755098818524));
#31827=CARTESIAN_POINT('Ctrl Pts',(0.117620974724197,-0.180236812191326,
1.14866963016836));
#31828=CARTESIAN_POINT('Ctrl Pts',(0.182356548323819,-0.0598586618003602,
1.1560820581571));
#31829=CARTESIAN_POINT('Ctrl Pts',(0.182115221868229,0.000725425160419088,
1.15978827215147));
#31830=CARTESIAN_POINT('Ctrl Pts',(-0.0861525859670525,0.175382131162755,
-1.38777878078145E-17));
#31831=CARTESIAN_POINT('Ctrl Pts',(-0.144496782441849,0.146721837385112,
0.00370621399437207));
#31832=CARTESIAN_POINT('Ctrl Pts',(-0.229323624142731,0.0270948940037977,
0.0111186419831162));
#31833=CARTESIAN_POINT('Ctrl Pts',(-0.14690228053469,-0.178453568564088,
0.0222372839662325));
#31834=CARTESIAN_POINT('Ctrl Pts',(0.0702798023147504,-0.219964250335881,
0.0333559259493488));
#31835=CARTESIAN_POINT('Ctrl Pts',(0.222983948348091,-0.0602620646924488,
0.044474567932465));
#31836=CARTESIAN_POINT('Ctrl Pts',(0.171476659751129,0.154790339194469,
0.0555932099155814));
#31837=CARTESIAN_POINT('Ctrl Pts',(-0.0371377304572895,0.22797075413722,
0.0667118518986976));
#31838=CARTESIAN_POINT('Ctrl Pts',(-0.211718147056775,0.0923606631345987,
0.0778304938818138));
#31839=CARTESIAN_POINT('Ctrl Pts',(-0.192363015131696,-0.12787712372945,
0.0889491358649302));
#31840=CARTESIAN_POINT('Ctrl Pts',(0.00320890232727887,-0.230962717925356,
0.100067777848046));
#31841=CARTESIAN_POINT('Ctrl Pts',(0.195839267869742,-0.122482325334233,
0.111186419831163));
#31842=CARTESIAN_POINT('Ctrl Pts',(0.209073448897961,0.0982002812028443,
0.122305061814279));
#31843=CARTESIAN_POINT('Ctrl Pts',(0.0307867124228199,0.228925546628532,
0.133423703797395));
#31844=CARTESIAN_POINT('Ctrl Pts',(-0.175701689972769,0.149945932314417,
0.144542345780511));
#31845=CARTESIAN_POINT('Ctrl Pts',(-0.221239878427269,-0.0663911091192784,
0.155660987763628));
#31846=CARTESIAN_POINT('Ctrl Pts',(-0.0641126576885465,-0.221910779030204,
0.166779629746744));
#31847=CARTESIAN_POINT('Ctrl Pts',(0.151744495713052,-0.174150671579767,
0.17789827172986));
#31848=CARTESIAN_POINT('Ctrl Pts',(0.228597130487397,0.0331390712847842,
0.189016913712977));
#31849=CARTESIAN_POINT('Ctrl Pts',(0.0960448643749269,0.210071953052146,
0.200135555696093));
#31850=CARTESIAN_POINT('Ctrl Pts',(-0.124488658037438,0.194569829998722,
0.211254197679209));
#31851=CARTESIAN_POINT('Ctrl Pts',(-0.230985172178094,0.000833292063536468,
0.222372839662325));
#31852=CARTESIAN_POINT('Ctrl Pts',(-0.12588924584139,-0.193666572611094,
0.233491481645442));
#31853=CARTESIAN_POINT('Ctrl Pts',(0.0945266903418065,-0.210759457362527,
0.244610123628558));
#31854=CARTESIAN_POINT('Ctrl Pts',(0.228352077714336,-0.0347875342430591,
0.255728765611674));
#31855=CARTESIAN_POINT('Ctrl Pts',(0.152997054850621,0.173051278744978,
0.26684740759479));
#31856=CARTESIAN_POINT('Ctrl Pts',(-0.0625099077306038,0.222367613142842,
0.277966049577907));
#31857=CARTESIAN_POINT('Ctrl Pts',(-0.220755082977362,0.0679855665342084,
0.289084691561023));
#31858=CARTESIAN_POINT('Ctrl Pts',(-0.176779024968342,-0.148674208393651,
0.300203333544139));
#31859=CARTESIAN_POINT('Ctrl Pts',(0.0291342892527361,-0.229141958423335,
0.311321975527256));
#31860=CARTESIAN_POINT('Ctrl Pts',(0.208359330569799,-0.0997057334412016,
0.322440617510372));
#31861=CARTESIAN_POINT('Ctrl Pts',(0.196718185643314,0.121065268979674,
0.333559259493488));
#31862=CARTESIAN_POINT('Ctrl Pts',(0.00487464827201324,0.230935232741881,
0.344677901476604));
#31863=CARTESIAN_POINT('Ctrl Pts',(-0.191434278399063,0.129258504441778,
0.355796543459721));
#31864=CARTESIAN_POINT('Ctrl Pts',(-0.212381100893932,-0.0908246216603541,
0.366915185442837));
#31865=CARTESIAN_POINT('Ctrl Pts',(-0.038777621054007,-0.227708453998192,
0.378033827425954));
#31866=CARTESIAN_POINT('Ctrl Pts',(0.170347841995286,-0.156001463596674,
0.389152469409069));
#31867=CARTESIAN_POINT('Ctrl Pts',(0.223427291426326,0.058609635407974,
0.400271111392186));
#31868=CARTESIAN_POINT('Ctrl Pts',(0.0718376487679439,0.219531765665651,
0.411389753375301));
#31869=CARTESIAN_POINT('Ctrl Pts',(-0.145558396757891,0.179353274433565,
0.422508395358419));
#31870=CARTESIAN_POINT('Ctrl Pts',(-0.229616635965357,-0.0251205972206891,
0.433627037341534));
#31871=CARTESIAN_POINT('Ctrl Pts',(-0.103336074967814,-0.206582911991821,
0.444745679324651));
#31872=CARTESIAN_POINT('Ctrl Pts',(0.117604813820203,-0.198806317010017,
0.455864321307767));
#31873=CARTESIAN_POINT('Ctrl Pts',(0.230814590995695,-0.00891451065749571,
0.466982963290884));
#31874=CARTESIAN_POINT('Ctrl Pts',(0.132588189186442,0.189143374203362,
0.478101605273999));
#31875=CARTESIAN_POINT('Ctrl Pts',(-0.0870947461077786,0.21393772252035,
0.489220247257116));
#31876=CARTESIAN_POINT('Ctrl Pts',(-0.226995115459196,0.0427558355600586,
0.500338889240232));
#31877=CARTESIAN_POINT('Ctrl Pts',(-0.158958111120973,-0.167592251687317,
0.511457531223348));
#31878=CARTESIAN_POINT('Ctrl Pts',(0.0546914192237968,-0.224418565586851,
0.522576173206465));
#31879=CARTESIAN_POINT('Ctrl Pts',(0.21824123683356,-0.0756677372605439,
0.533694815189581));
#31880=CARTESIAN_POINT('Ctrl Pts',(0.181872613351991,0.14239802115651,0.544813457172697));
#31881=CARTESIAN_POINT('Ctrl Pts',(-0.0210992142997687,0.230021014415434,
0.555932099155813));
#31882=CARTESIAN_POINT('Ctrl Pts',(-0.204743246287144,0.106934779265563,
0.567050741138931));
#31883=CARTESIAN_POINT('Ctrl Pts',(-0.200833582118916,-0.114108352937273,
0.578169383122044));
#31884=CARTESIAN_POINT('Ctrl Pts',(-0.0129516437895867,-0.230623283386393,
0.589288025105164));
#31885=CARTESIAN_POINT('Ctrl Pts',(0.186794562143574,-0.135877280920554,
0.600406667088277));
#31886=CARTESIAN_POINT('Ctrl Pts',(0.215428845280213,0.083338205752262,
0.611525309071395));
#31887=CARTESIAN_POINT('Ctrl Pts',(0.0467209600008474,0.226212280421227,
0.622643951054511));
#31888=CARTESIAN_POINT('Ctrl Pts',(-0.164785351575852,0.161866092257753,
0.633762593037627));
#31889=CARTESIAN_POINT('Ctrl Pts',(-0.225341132081031,-0.0507564587930634,
0.644881235020743));
#31890=CARTESIAN_POINT('Ctrl Pts',(-0.0794746594271866,-0.21688389157728,
0.655999877003859));
#31891=CARTESIAN_POINT('Ctrl Pts',(0.139194049181108,-0.184336270411821,
0.667118518986976));
#31892=CARTESIAN_POINT('Ctrl Pts',(0.230354969961477,0.0170713716736379,
0.678237160970093));
#31893=CARTESIAN_POINT('Ctrl Pts',(0.11050074456459,0.202840896683692,0.689355802953208));
#31894=CARTESIAN_POINT('Ctrl Pts',(-0.110576956804586,0.202799360306213,
0.700474444936325));
#31895=CARTESIAN_POINT('Ctrl Pts',(-0.230361368483253,0.0169848116649841,
0.711593086919441));
#31896=CARTESIAN_POINT('Ctrl Pts',(-0.139124772661127,-0.184388561328419,
0.722711728902557));
#31897=CARTESIAN_POINT('Ctrl Pts',(0.0795561506911461,-0.216854012653626,
0.733830370885674));
#31898=CARTESIAN_POINT('Ctrl Pts',(0.225360188555757,-0.0506717804195071,
0.744949012868789));
#31899=CARTESIAN_POINT('Ctrl Pts',(0.164724516703786,0.161928001017393,
0.756067654851907));
#31900=CARTESIAN_POINT('Ctrl Pts',(-0.0468059588377044,0.226194708457211,
0.767186296835021));
#31901=CARTESIAN_POINT('Ctrl Pts',(-0.2154601454596,0.0832572497460946,
0.778304938818139));
#31902=CARTESIAN_POINT('Ctrl Pts',(-0.18674349134348,-0.135947461755279,
0.789423580801255));
#31903=CARTESIAN_POINT('Ctrl Pts',(0.0130383025010703,-0.230618400359892,
0.800542222784371));
#31904=CARTESIAN_POINT('Ctrl Pts',(0.200876445601631,-0.114032879114536,
0.811660864767487));
#31905=CARTESIAN_POINT('Ctrl Pts',(0.204703049732954,0.107011706590215,
0.822779506750604));
#31906=CARTESIAN_POINT('Ctrl Pts',(0.0210127794931219,0.230028926472067,
0.83389814873372));
#31907=CARTESIAN_POINT('Ctrl Pts',(-0.181926108372479,0.142329670163983,
0.845016790716836));
#31908=CARTESIAN_POINT('Ctrl Pts',(-0.218212788319439,-0.0757497388391501,
0.856135432699953));
#31909=CARTESIAN_POINT('Ctrl Pts',(-0.0546070872270015,-0.224439100726275,
0.867254074683069));
#31910=CARTESIAN_POINT('Ctrl Pts',(0.159021074792356,-0.167532509350284,
0.878372716666185));
#31911=CARTESIAN_POINT('Ctrl Pts',(0.226979033427429,0.0428411288796547,
0.889491358649301));
#31912=CARTESIAN_POINT('Ctrl Pts',(0.0870143500653468,0.213970434291613,
0.900610000632417));
#31913=CARTESIAN_POINT('Ctrl Pts',(-0.132659252698235,0.189093539309814,
0.911728642615534));
#31914=CARTESIAN_POINT('Ctrl Pts',(-0.230811225247311,-0.00900124183420705,
0.92284728459865));
#31915=CARTESIAN_POINT('Ctrl Pts',(-0.117530100973675,-0.198850493915805,
0.933965926581767));
#31916=CARTESIAN_POINT('Ctrl Pts',(0.103413692781901,-0.206544068631896,
0.945084568564882));
#31917=CARTESIAN_POINT('Ctrl Pts',(0.229626061120593,-0.0250343120523647,
0.956203210547999));
#31918=CARTESIAN_POINT('Ctrl Pts',(0.145490988438074,0.179407953322179,
0.967321852531115));
#31919=CARTESIAN_POINT('Ctrl Pts',(-0.0719201283577143,0.219504763615053,
0.978440494514231));
#31920=CARTESIAN_POINT('Ctrl Pts',(-0.22344931264651,0.0585256616254353,
0.989559136497349));
#31921=CARTESIAN_POINT('Ctrl Pts',(-0.170289184396906,-0.156065436285928,
1.00067777848046));
#31922=CARTESIAN_POINT('Ctrl Pts',(0.0388631330803271,-0.227693917494037,
1.01179642046358));
#31923=CARTESIAN_POINT('Ctrl Pts',(0.21241530878674,-0.0907447137301155,
1.0229150624467));
#31924=CARTESIAN_POINT('Ctrl Pts',(0.191385514681521,0.129330245229283,
1.03403370442981));
#31925=CARTESIAN_POINT('Ctrl Pts',(-0.00496108271125438,0.230933734912719,
1.04515234641293));
#31926=CARTESIAN_POINT('Ctrl Pts',(-0.196764314760194,0.120990674417448,
1.05627098839605));
#31927=CARTESIAN_POINT('Ctrl Pts',(-0.208320610464741,-0.0997827509202423,
1.06738963037916));
#31928=CARTESIAN_POINT('Ctrl Pts',(-0.0290505442625618,-0.229155305943203,
1.07850827236228));
#31929=CARTESIAN_POINT('Ctrl Pts',(0.17683937169233,-0.148603171255794,
1.08962691434539));
#31930=CARTESIAN_POINT('Ctrl Pts',(0.220720967111538,0.0680597564112484,
1.10074555632851));
#31931=CARTESIAN_POINT('Ctrl Pts',(0.0624426335084105,0.222407759459687,
1.11186419831163));
#31932=CARTESIAN_POINT('Ctrl Pts',(-0.153093107010227,0.172962013887028,
1.12298284029474));
#31933=CARTESIAN_POINT('Ctrl Pts',(-0.228279649924591,-0.0348126912135875,
1.13410148227786));
#31934=CARTESIAN_POINT('Ctrl Pts',(-0.0945626503816835,-0.210911975270116,
1.14522012426097));
#31935=CARTESIAN_POINT('Ctrl Pts',(0.126200083066393,-0.193383031585166,
1.15633876624409));
#31936=CARTESIAN_POINT('Ctrl Pts',(0.195657378287586,-0.0642246683396576,
1.16375119423284));
#31937=CARTESIAN_POINT('Ctrl Pts',(0.195398449819998,0.00077833665056624,
1.16745740822721));
#31938=CARTESIAN_POINT('Ctrl Pts',(-0.195093054978418,-5.50606481354719E-5,
1.06241303078758));
#31939=CARTESIAN_POINT('Ctrl Pts',(-0.195166977968097,-0.0292567552961119,
1.0640718973181));
#31940=CARTESIAN_POINT('Ctrl Pts',(-0.189027401228485,-0.0584289311968449,
1.06573076384863));
#31941=CARTESIAN_POINT('Ctrl Pts',(-0.17651621681362,-0.0845492725344543,
1.06738963037916));
#31942=CARTESIAN_POINT('Ctrl Pts',(-0.148563921730681,-0.142906935927896,
1.07109584437353));
#31943=CARTESIAN_POINT('Ctrl Pts',(-0.0888072329966215,-0.18603112093555,
1.07480205836791));
#31944=CARTESIAN_POINT('Ctrl Pts',(-0.0246139026371096,-0.194167857658142,
1.07850827236228));
#31945=CARTESIAN_POINT('Ctrl Pts',(0.0395794277224022,-0.202304594380734,
1.08221448635665));
#31946=CARTESIAN_POINT('Ctrl Pts',(0.108209399707366,-0.175453882818264,
1.08592070035102));
#31947=CARTESIAN_POINT('Ctrl Pts',(0.149837984936383,-0.125918039092522,
1.08962691434539));
#31948=CARTESIAN_POINT('Ctrl Pts',(0.191466570165399,-0.0763821953667804,
1.09333312833977));
#31949=CARTESIAN_POINT('Ctrl Pts',(0.206093768638468,-0.0041612194777677,
1.09703934233414));
#31950=CARTESIAN_POINT('Ctrl Pts',(0.187027645607817,0.0576739356414784,
1.10074555632851));
#31951=CARTESIAN_POINT('Ctrl Pts',(0.180418088670294,0.0791100177355746,
1.10203037088567));
#31952=CARTESIAN_POINT('Ctrl Pts',(0.169759382901609,0.0992979671982257,
1.10331518544284));
#31953=CARTESIAN_POINT('Ctrl Pts',(0.156057659382855,0.117255425406022,
1.1046));
#31954=CARTESIAN_POINT('Ctrl Pts',(-0.09055496143049,-0.12679201530598,
5.09575021068187E-18));
#31955=CARTESIAN_POINT('Ctrl Pts',(-0.0937460871048188,-0.125085822491965,
4.58984227758833E-18));
#31956=CARTESIAN_POINT('Ctrl Pts',(-0.0968677330061127,-0.123263760516135,
2.50662287286079E-17));
#31957=CARTESIAN_POINT('Ctrl Pts',(-0.0999128467894991,-0.121327242330634,
2.00577401909818E-17));
#31958=CARTESIAN_POINT('Ctrl Pts',(-0.107335152566795,-0.11660708041271,
6.42545598945985E-18));
#31959=CARTESIAN_POINT('Ctrl Pts',(-0.11430344392066,-0.111208610599775,
9.99023806675092E-18));
#31960=CARTESIAN_POINT('Ctrl Pts',(-0.120790707516777,-0.105232728283189,
2.60208521396521E-17));
#31961=CARTESIAN_POINT('Ctrl Pts',(-0.123891078118351,-0.102376755255687,
3.36821478247169E-17));
#31962=CARTESIAN_POINT('Ctrl Pts',(-0.126881418116351,-0.099388034385428,
-1.92452104322545E-17));
#31963=CARTESIAN_POINT('Ctrl Pts',(-0.129748204847616,-0.0962880923092239,
-1.51788304147971E-17));
#31964=CARTESIAN_POINT('Ctrl Pts',(-0.135037647654988,-0.0905684598931024,
-7.67604539740766E-18));
#31965=CARTESIAN_POINT('Ctrl Pts',(-0.139916189540312,-0.0844627163539483,
6.65058155921973E-18));
#31966=CARTESIAN_POINT('Ctrl Pts',(-0.144364609008094,-0.0780350740853688,
-6.07153216591882E-18));
#31967=CARTESIAN_POINT('Ctrl Pts',(-0.146693883418799,-0.0746694421422029,
-1.2733065360948E-17));
#31968=CARTESIAN_POINT('Ctrl Pts',(-0.148905919766188,-0.0712140221787596,
5.51914947350105E-18));
#31969=CARTESIAN_POINT('Ctrl Pts',(-0.150994732263837,-0.0676811328914676,
3.46944695195361E-18));
#31970=CARTESIAN_POINT('Ctrl Pts',(-0.156930492501974,-0.0576417522477531,
-2.35517480854577E-18));
#31971=CARTESIAN_POINT('Ctrl Pts',(-0.161837586723136,-0.04704232833817,
1.0498384979768E-17));
#31972=CARTESIAN_POINT('Ctrl Pts',(-0.165656700638674,-0.0360824270657778,
6.93889390390723E-18));
#31973=CARTESIAN_POINT('Ctrl Pts',(-0.168566598677898,-0.0277317478433351,
4.22681033390876E-18));
#31974=CARTESIAN_POINT('Ctrl Pts',(-0.17084455406887,-0.0191704748820838,
-1.37633633951559E-17));
#31975=CARTESIAN_POINT('Ctrl Pts',(-0.172449224480544,-0.0104741012692795,
-1.56125112837913E-17));
#31976=CARTESIAN_POINT('Ctrl Pts',(-0.173092222694612,-0.00698942761839798,
-1.63534726558537E-17));
#31977=CARTESIAN_POINT('Ctrl Pts',(-0.173626618765139,-0.00348302750915761,
-1.21488779396688E-17));
#31978=CARTESIAN_POINT('Ctrl Pts',(-0.174048178602262,2.59546856150664E-5,
-1.38777878078145E-17));
#31979=CARTESIAN_POINT('Ctrl Pts',(-0.174866886128293,0.00684071709555691,
-1.72354879401115E-17));
#31980=CARTESIAN_POINT('Ctrl Pts',(-0.175263001859704,0.0136781916586682,
-1.47570089434246E-17));
#31981=CARTESIAN_POINT('Ctrl Pts',(-0.175222496230419,0.020502014676713,
-1.73472347597681E-17));
#31982=CARTESIAN_POINT('Ctrl Pts',(-0.175176789703203,0.0282020123806742,
-2.02700439806174E-17));
#31983=CARTESIAN_POINT('Ctrl Pts',(-0.174575488437737,0.0358847565960055,
-4.14656083691159E-17));
#31984=CARTESIAN_POINT('Ctrl Pts',(-0.173454133268089,0.0435109284941294,
-3.81639164714898E-17));
#31985=CARTESIAN_POINT('Ctrl Pts',(-0.172772227559337,0.0481484691182048,
-3.61561292739328E-17));
#31986=CARTESIAN_POINT('Ctrl Pts',(-0.171897804056446,0.0527651363053484,
-4.88916554017709E-17));
#31987=CARTESIAN_POINT('Ctrl Pts',(-0.170837068741884,0.0573521982187067,
-5.03069808033274E-17));
#31988=CARTESIAN_POINT('Ctrl Pts',(-0.170031029630167,0.0608378475218587,
-5.1382468357856E-17));
#31989=CARTESIAN_POINT('Ctrl Pts',(-0.169117246541092,0.0643057763689402,
-8.52354934901958E-18));
#31990=CARTESIAN_POINT('Ctrl Pts',(-0.168102750715484,0.0677391082731898,
-8.67361737988404E-18));
#31991=CARTESIAN_POINT('Ctrl Pts',(-0.164848133533702,0.0787536247692379,
-9.1550525709997E-18));
#31992=CARTESIAN_POINT('Ctrl Pts',(-0.160552714845615,0.0894467883889295,
-1.4615508474092E-17));
#31993=CARTESIAN_POINT('Ctrl Pts',(-0.155326482610649,0.0996955319262882,
-3.12250225675825E-17));
#31994=CARTESIAN_POINT('Ctrl Pts',(-0.152120282364142,0.105982953261303,
-4.14146631703528E-17));
#31995=CARTESIAN_POINT('Ctrl Pts',(-0.148562901683281,0.112103241720107,
-3.61201279282247E-17));
#31996=CARTESIAN_POINT('Ctrl Pts',(-0.144672442230625,0.118026999364952,
-4.16333634234434E-17));
#31997=CARTESIAN_POINT('Ctrl Pts',(-0.141744976772053,0.122484466690154,
-4.57819239401724E-17));
#31998=CARTESIAN_POINT('Ctrl Pts',(-0.138624730042886,0.126835138052646,
-6.23512024481927E-18));
#31999=CARTESIAN_POINT('Ctrl Pts',(-0.135339728450536,0.131039395408961,
-6.93889390390723E-18));
#32000=CARTESIAN_POINT('Ctrl Pts',(-0.127443588741529,0.141145144987709,
-8.63055065945266E-18));
#32001=CARTESIAN_POINT('Ctrl Pts',(-0.118584883784043,0.150432575075823,
-5.34207396488032E-18));
#32002=CARTESIAN_POINT('Ctrl Pts',(-0.108881311648901,0.158738497602418,
0.));
#32003=CARTESIAN_POINT('Ctrl Pts',(-0.101751737768341,0.16484116654483,
3.92501961933201E-18));
#32004=CARTESIAN_POINT('Ctrl Pts',(-0.0941648935161059,0.170414009123921,
-1.10648570806265E-17));
#32005=CARTESIAN_POINT('Ctrl Pts',(-0.0861525859670525,0.175382131162755,
-1.38777878078145E-17));
#32006=CARTESIAN_POINT('Origin',(0.,0.,0.));
#32007=CARTESIAN_POINT('Origin',(-0.0866025403784439,-0.15,-0.4));
#32008=CARTESIAN_POINT('',(-0.0866025403784439,-0.15,-0.4));
#32009=CARTESIAN_POINT('',(0.0866025403784439,-0.15,-0.4));
#32010=CARTESIAN_POINT('',(-0.043301270189222,-0.15,-0.4));
#32011=CARTESIAN_POINT('',(-0.0866025403784439,-0.15,-0.2));
#32012=CARTESIAN_POINT('',(-0.0866025403784439,-0.15,-0.4));
#32013=CARTESIAN_POINT('',(0.0866025403784439,-0.15,-0.2));
#32014=CARTESIAN_POINT('',(-0.0866025403784439,-0.15,-0.2));
#32015=CARTESIAN_POINT('',(0.0866025403784439,-0.15,-0.4));
#32016=CARTESIAN_POINT('Origin',(-0.173205080756888,2.12115047744981E-17,
-0.4));
#32017=CARTESIAN_POINT('',(-0.173205080756888,2.12115047744981E-17,-0.4));
#32018=CARTESIAN_POINT('',(-0.151554445662277,-0.0375,-0.4));
#32019=CARTESIAN_POINT('',(-0.173205080756888,2.77555756156289E-17,-0.2));
#32020=CARTESIAN_POINT('',(-0.173205080756888,2.12115047744981E-17,-0.4));
#32021=CARTESIAN_POINT('',(-0.173205080756888,2.12115047744981E-17,-0.2));
#32022=CARTESIAN_POINT('Origin',(-0.0866025403784438,0.15,-0.4));
#32023=CARTESIAN_POINT('',(-0.0866025403784438,0.15,-0.4));
#32024=CARTESIAN_POINT('',(-0.108253175473055,0.1125,-0.4));
#32025=CARTESIAN_POINT('',(-0.0866025403784438,0.15,-0.2));
#32026=CARTESIAN_POINT('',(-0.0866025403784438,0.15,-0.4));
#32027=CARTESIAN_POINT('',(-0.0866025403784438,0.15,-0.2));
#32028=CARTESIAN_POINT('Origin',(0.0866025403784439,0.15,-0.4));
#32029=CARTESIAN_POINT('',(0.0866025403784439,0.15,-0.4));
#32030=CARTESIAN_POINT('',(0.043301270189222,0.15,-0.4));
#32031=CARTESIAN_POINT('',(0.0866025403784439,0.15,-0.2));
#32032=CARTESIAN_POINT('',(0.0866025403784439,0.15,-0.4));
#32033=CARTESIAN_POINT('',(0.0866025403784439,0.15,-0.2));
#32034=CARTESIAN_POINT('Origin',(0.173205080756888,0.,-0.4));
#32035=CARTESIAN_POINT('',(0.173205080756888,0.,-0.4));
#32036=CARTESIAN_POINT('',(0.151554445662277,0.0375,-0.4));
#32037=CARTESIAN_POINT('',(0.173205080756888,0.,-0.2));
#32038=CARTESIAN_POINT('',(0.173205080756888,0.,-0.4));
#32039=CARTESIAN_POINT('',(0.173205080756888,0.,-0.2));
#32040=CARTESIAN_POINT('Origin',(0.0866025403784439,-0.15,-0.4));
#32041=CARTESIAN_POINT('',(0.108253175473055,-0.1125,-0.4));
#32042=CARTESIAN_POINT('',(0.0866025403784439,-0.15,-0.2));
#32043=CARTESIAN_POINT('Origin',(0.,2.77555756156289E-17,-0.2));
#32044=CARTESIAN_POINT('Origin',(0.,0.,0.));
#32045=CARTESIAN_POINT('',(-0.35,-4.28626379701574E-17,0.));
#32046=CARTESIAN_POINT('Origin',(0.,0.,0.));
#32047=CARTESIAN_POINT('Origin',(0.,0.,-0.4));
#32048=CARTESIAN_POINT('',(-0.35,-4.28626379701574E-17,-0.4));
#32049=CARTESIAN_POINT('',(-0.35,-4.28626379701574E-17,-0.4));
#32050=CARTESIAN_POINT('Origin',(0.,0.,-0.4));
#32051=CARTESIAN_POINT('Origin',(0.,0.,-0.4));
#32052=CARTESIAN_POINT('Origin',(0.,0.,1.2));
#36460=UNCERTAINTY_MEASURE_WITH_UNIT(LENGTH_MEASURE(0.001),#36483,
'DISTANCE_ACCURACY_VALUE',
'Maximum model space distance between geometric entities at asserted c
onnectivities');
#36463=UNCERTAINTY_MEASURE_WITH_UNIT(LENGTH_MEASURE(0.001),#36483,
'DISTANCE_ACCURACY_VALUE',
'Maximum model space distance between geometric entities at asserted c
onnectivities');
#36479=(
GEOMETRIC_REPRESENTATION_CONTEXT(3)
GLOBAL_UNCERTAINTY_ASSIGNED_CONTEXT((#36460))
GLOBAL_UNIT_ASSIGNED_CONTEXT((#36483,#36485,#36486))
REPRESENTATION_CONTEXT('','3D')
);
#36482=(
GEOMETRIC_REPRESENTATION_CONTEXT(3)
GLOBAL_UNCERTAINTY_ASSIGNED_CONTEXT((#36463))
GLOBAL_UNIT_ASSIGNED_CONTEXT((#36483,#36485,#36486))
REPRESENTATION_CONTEXT('','3D')
);
#36483=(
LENGTH_UNIT()
NAMED_UNIT(*)
SI_UNIT(.CENTI.,.METRE.)
);
#36485=(
NAMED_UNIT(*)
PLANE_ANGLE_UNIT()
SI_UNIT($,.RADIAN.)
);
#36486=(
NAMED_UNIT(*)
SI_UNIT($,.STERADIAN.)
SOLID_ANGLE_UNIT()
);
#36502=SHAPE_DEFINITION_REPRESENTATION(#36520,#36569);
#36520=PRODUCT_DEFINITION_SHAPE('',$,#36588);
#36569=SHAPE_REPRESENTATION('',(#10505),#36479);
#36572=PRODUCT_DEFINITION_CONTEXT('part definition',#36628,'design');
#36588=PRODUCT_DEFINITION('Socket head cap screw M4x12',
'Socket head cap screw M4x12',#36606,#36572);
#36606=PRODUCT_DEFINITION_FORMATION('',$,#36645);
#36628=APPLICATION_CONTEXT(
'Core Data for Automotive Mechanical Design Process');
#36629=PRODUCT_CONTEXT('part definition',#36628,'mechanical');
#36645=PRODUCT('Socket head cap screw M4x12',
'Socket head cap screw M4x12',$,(#36629));
#36659=PRESENTATION_STYLE_ASSIGNMENT((#36673));
#36673=SURFACE_STYLE_USAGE(.BOTH.,#36687);
#36687=SURFACE_SIDE_STYLE('',(#36701));
#36701=SURFACE_STYLE_FILL_AREA(#36715);
#36715=FILL_AREA_STYLE('Dark gray',(#36729));
#36729=FILL_AREA_STYLE_COLOUR('Dark gray',#36743);
#36743=COLOUR_RGB('Dark gray',0.250980392156863,0.282352941176471,0.32156862745098);
ENDSEC;
END-ISO-10303-21;
